ISO-10303-21;
HEADER;
/* Generated by software containing ST-Developer
 * from STEP Tools, Inc. (www.steptools.com) 
 */

FILE_DESCRIPTION(
/* description */ ('Independent hinged machine back cover with retained hinge pins, perim
eter gasket and quarter-turn cam latch. Nominal cover 360 x 260 x 3 mm
, frame 430 x 300 x 20 mm. No guarding, structural or ingress rating a
ssigned.'),
/* implementation_level */ '2;1');

FILE_NAME(
/* name */ 'Socket head cap screw M6x12.step',
/* time_stamp */ '2026-11-09T19:36:59-08:00',
/* author */ (''),
/* organization */ (''),
/* preprocessor_version */ 'ST-DEVELOPER v20.2',
/* originating_system */ 'Autodesk Translation Framework v15.17.0.0',
/* authorisation */ '');

FILE_SCHEMA (('AUTOMOTIVE_DESIGN { 1 0 10303 214 3 1 1 }'));
ENDSEC;

DATA;
#10=MECHANICAL_DESIGN_GEOMETRIC_PRESENTATION_REPRESENTATION('',(#213),#32627);
#161=CONICAL_SURFACE('',#9439,2.5,0.785398163397449);
#177=SHAPE_REPRESENTATION_RELATIONSHIP('SRR','None',#32723,#195);
#195=ADVANCED_BREP_SHAPE_REPRESENTATION('',(#231),#32624);
#213=STYLED_ITEM('',(#32809),#231);
#231=MANIFOLD_SOLID_BREP('Body1',#8690);
#287=FACE_BOUND('',#1426,.T.);
#288=FACE_BOUND('',#1429,.T.);
#307=B_SPLINE_SURFACE_WITH_KNOTS('',3,3,((#30530,#30531,#30532,#30533,#30534,
#30535,#30536,#30537,#30538,#30539,#30540,#30541,#30542,#30543,#30544,#30545,
#30546,#30547,#30548,#30549,#30550,#30551,#30552,#30553,#30554,#30555,#30556,
#30557,#30558,#30559,#30560,#30561,#30562,#30563,#30564,#30565,#30566,#30567,
#30568,#30569,#30570,#30571,#30572,#30573,#30574,#30575,#30576,#30577,#30578,
#30579,#30580,#30581,#30582,#30583,#30584,#30585,#30586,#30587,#30588,#30589,
#30590,#30591,#30592,#30593,#30594,#30595,#30596,#30597,#30598,#30599,#30600,
#30601,#30602,#30603,#30604,#30605,#30606),(#30607,#30608,#30609,#30610,
#30611,#30612,#30613,#30614,#30615,#30616,#30617,#30618,#30619,#30620,#30621,
#30622,#30623,#30624,#30625,#30626,#30627,#30628,#30629,#30630,#30631,#30632,
#30633,#30634,#30635,#30636,#30637,#30638,#30639,#30640,#30641,#30642,#30643,
#30644,#30645,#30646,#30647,#30648,#30649,#30650,#30651,#30652,#30653,#30654,
#30655,#30656,#30657,#30658,#30659,#30660,#30661,#30662,#30663,#30664,#30665,
#30666,#30667,#30668,#30669,#30670,#30671,#30672,#30673,#30674,#30675,#30676,
#30677,#30678,#30679,#30680,#30681,#30682,#30683),(#30684,#30685,#30686,
#30687,#30688,#30689,#30690,#30691,#30692,#30693,#30694,#30695,#30696,#30697,
#30698,#30699,#30700,#30701,#30702,#30703,#30704,#30705,#30706,#30707,#30708,
#30709,#30710,#30711,#30712,#30713,#30714,#30715,#30716,#30717,#30718,#30719,
#30720,#30721,#30722,#30723,#30724,#30725,#30726,#30727,#30728,#30729,#30730,
#30731,#30732,#30733,#30734,#30735,#30736,#30737,#30738,#30739,#30740,#30741,
#30742,#30743,#30744,#30745,#30746,#30747,#30748,#30749,#30750,#30751,#30752,
#30753,#30754,#30755,#30756,#30757,#30758,#30759,#30760),(#30761,#30762,
#30763,#30764,#30765,#30766,#30767,#30768,#30769,#30770,#30771,#30772,#30773,
#30774,#30775,#30776,#30777,#30778,#30779,#30780,#30781,#30782,#30783,#30784,
#30785,#30786,#30787,#30788,#30789,#30790,#30791,#30792,#30793,#30794,#30795,
#30796,#30797,#30798,#30799,#30800,#30801,#30802,#30803,#30804,#30805,#30806,
#30807,#30808,#30809,#30810,#30811,#30812,#30813,#30814,#30815,#30816,#30817,
#30818,#30819,#30820,#30821,#30822,#30823,#30824,#30825,#30826,#30827,#30828,
#30829,#30830,#30831,#30832,#30833,#30834,#30835,#30836,#30837)),
 .UNSPECIFIED.,.F.,.F.,.F.,(4,4),(4,1,1,1,1,1,1,1,1,1,1,1,1,1,1,1,1,1,1,
1,1,1,1,1,1,1,1,1,1,1,1,1,1,1,1,1,1,1,1,1,1,1,1,1,1,1,1,1,1,1,1,1,1,1,1,
1,1,1,1,1,1,1,1,1,1,1,1,1,1,1,1,1,1,1,4),(0.,0.0658467982010768),(11.6150328478182,
12.6023632471184,13.5896936464185,14.5770240457187,15.5643544450188,16.551684844319,
17.5390152436191,18.5263456429193,19.5136760422194,20.5010064415196,21.4883368408197,
22.4756672401199,23.46299763942,24.4503280387202,25.4376584380203,26.4249888373205,
27.4123192366206,28.3996496359208,29.3869800352209,30.3743104345211,31.3616408338212,
32.3489712331214,33.3363016324215,34.3236320317217,35.3109624310218,36.298292830322,
37.2856232296221,38.2729536289223,39.2602840282224,40.2476144275226,41.2349448268227,
42.2222752261229,43.209605625423,44.1969360247232,45.1842664240233,46.1715968233235,
47.1589272226236,48.1462576219238,49.1335880212239,50.1209184205241,51.1082488198242,
52.0955792191244,53.0829096184245,54.0702400177247,55.0575704170248,56.0449008163249,
57.0322312156251,58.0195616149252,59.0068920142254,59.9942224135255,60.9815528128257,
61.9688832121258,62.956213611426,63.9435440107261,64.9308744100263,65.9182048093264,
66.9055352086266,67.8928656079267,68.8801960072269,69.867526406527,70.8548568058272,
71.8421872051273,72.8295176044275,73.8168480037276,74.8041784030278,75.7915088023279,
76.7788392016281,77.7661696009282,78.7535000002284,79.7408303995285,80.7281607988287,
81.7154911981288,82.702821597429,83.6901519967291,84.6774823960293),
 .UNSPECIFIED.);
#308=B_SPLINE_SURFACE_WITH_KNOTS('',3,3,((#30966,#30967,#30968,#30969,#30970,
#30971,#30972,#30973,#30974,#30975,#30976,#30977,#30978,#30979,#30980,#30981,
#30982,#30983,#30984,#30985,#30986,#30987,#30988,#30989,#30990,#30991,#30992,
#30993,#30994,#30995,#30996,#30997,#30998,#30999,#31000,#31001,#31002,#31003,
#31004,#31005,#31006,#31007,#31008,#31009,#31010,#31011,#31012,#31013,#31014,
#31015,#31016,#31017,#31018,#31019,#31020,#31021,#31022,#31023,#31024,#31025,
#31026,#31027,#31028,#31029,#31030,#31031,#31032,#31033,#31034,#31035,#31036,
#31037,#31038,#31039,#31040,#31041,#31042,#31043,#31044),(#31045,#31046,
#31047,#31048,#31049,#31050,#31051,#31052,#31053,#31054,#31055,#31056,#31057,
#31058,#31059,#31060,#31061,#31062,#31063,#31064,#31065,#31066,#31067,#31068,
#31069,#31070,#31071,#31072,#31073,#31074,#31075,#31076,#31077,#31078,#31079,
#31080,#31081,#31082,#31083,#31084,#31085,#31086,#31087,#31088,#31089,#31090,
#31091,#31092,#31093,#31094,#31095,#31096,#31097,#31098,#31099,#31100,#31101,
#31102,#31103,#31104,#31105,#31106,#31107,#31108,#31109,#31110,#31111,#31112,
#31113,#31114,#31115,#31116,#31117,#31118,#31119,#31120,#31121,#31122,#31123),
(#31124,#31125,#31126,#31127,#31128,#31129,#31130,#31131,#31132,#31133,
#31134,#31135,#31136,#31137,#31138,#31139,#31140,#31141,#31142,#31143,#31144,
#31145,#31146,#31147,#31148,#31149,#31150,#31151,#31152,#31153,#31154,#31155,
#31156,#31157,#31158,#31159,#31160,#31161,#31162,#31163,#31164,#31165,#31166,
#31167,#31168,#31169,#31170,#31171,#31172,#31173,#31174,#31175,#31176,#31177,
#31178,#31179,#31180,#31181,#31182,#31183,#31184,#31185,#31186,#31187,#31188,
#31189,#31190,#31191,#31192,#31193,#31194,#31195,#31196,#31197,#31198,#31199,
#31200,#31201,#31202),(#31203,#31204,#31205,#31206,#31207,#31208,#31209,
#31210,#31211,#31212,#31213,#31214,#31215,#31216,#31217,#31218,#31219,#31220,
#31221,#31222,#31223,#31224,#31225,#31226,#31227,#31228,#31229,#31230,#31231,
#31232,#31233,#31234,#31235,#31236,#31237,#31238,#31239,#31240,#31241,#31242,
#31243,#31244,#31245,#31246,#31247,#31248,#31249,#31250,#31251,#31252,#31253,
#31254,#31255,#31256,#31257,#31258,#31259,#31260,#31261,#31262,#31263,#31264,
#31265,#31266,#31267,#31268,#31269,#31270,#31271,#31272,#31273,#31274,#31275,
#31276,#31277,#31278,#31279,#31280,#31281)),.UNSPECIFIED.,.F.,.F.,.F.,(4,
4),(4,1,1,1,1,1,1,1,1,1,1,1,1,1,1,1,1,1,1,1,1,1,1,1,1,1,1,1,1,1,1,1,1,1,
1,1,1,1,1,1,1,1,1,1,1,1,1,1,1,1,1,1,1,1,1,1,1,1,1,1,1,1,1,1,1,1,1,1,1,1,
1,1,1,1,1,1,4),(0.,0.0658467982010768),(8.30747755240104,9.2960444961263,
10.2846114398516,11.2731783835768,12.2617453273021,13.2503122710274,14.2388792147526,
15.2274461584779,16.2160131022032,17.2045800459284,18.1931469896537,19.181713933379,
20.1702808771042,21.1588478208295,22.1474147645547,23.13598170828,24.1245486520053,
25.1131155957305,26.1016825394558,27.0902494831811,28.0788164269063,29.0673833706316,
30.0559503143569,31.0445172580821,32.0330842018074,33.0216511455327,34.0102180892579,
34.9987850329832,35.9873519767085,36.9759189204337,37.964485864159,38.9530528078842,
39.9416197516095,40.9301866953348,41.91875363906,42.9073205827853,43.8958875265106,
44.8844544702358,45.8730214139611,46.8615883576864,47.8501553014116,48.8387222451369,
49.8272891888622,50.8158561325874,51.8044230763127,52.792990020038,53.7815569637632,
54.7701239074885,55.7586908512138,56.747257794939,57.7358247386643,58.7243916823895,
59.7129586261148,60.7015255698401,61.6900925135653,62.6786594572906,63.6672264010159,
64.6557933447411,65.6443602884664,66.6329272321917,67.6214941759169,68.6100611196422,
69.5986280633675,70.5871950070927,71.575761950818,72.5643288945433,73.5528958382685,
74.5414627819938,75.530029725719,76.5185966694443,77.5071636131696,78.4957305568948,
79.4842975006201,80.4728644443454,81.4614313880706,82.4499983317959,83.4385652755212),
 .UNSPECIFIED.);
#432=PLANE('',#9445);
#433=PLANE('',#9446);
#434=PLANE('',#9447);
#435=PLANE('',#9448);
#436=PLANE('',#9449);
#437=PLANE('',#9450);
#438=PLANE('',#9451);
#439=PLANE('',#9452);
#440=PLANE('',#9456);
#441=PLANE('',#9457);
#863=FACE_OUTER_BOUND('',#1391,.T.);
#864=FACE_OUTER_BOUND('',#1392,.T.);
#865=FACE_OUTER_BOUND('',#1393,.T.);
#866=FACE_OUTER_BOUND('',#1394,.T.);
#867=FACE_OUTER_BOUND('',#1395,.T.);
#868=FACE_OUTER_BOUND('',#1396,.T.);
#869=FACE_OUTER_BOUND('',#1397,.T.);
#870=FACE_OUTER_BOUND('',#1398,.T.);
#871=FACE_OUTER_BOUND('',#1399,.T.);
#872=FACE_OUTER_BOUND('',#1400,.T.);
#873=FACE_OUTER_BOUND('',#1401,.T.);
#874=FACE_OUTER_BOUND('',#1402,.T.);
#875=FACE_OUTER_BOUND('',#1403,.T.);
#876=FACE_OUTER_BOUND('',#1404,.T.);
#877=FACE_OUTER_BOUND('',#1405,.T.);
#878=FACE_OUTER_BOUND('',#1406,.T.);
#879=FACE_OUTER_BOUND('',#1407,.T.);
#880=FACE_OUTER_BOUND('',#1408,.T.);
#881=FACE_OUTER_BOUND('',#1409,.T.);
#882=FACE_OUTER_BOUND('',#1410,.T.);
#883=FACE_OUTER_BOUND('',#1411,.T.);
#884=FACE_OUTER_BOUND('',#1412,.T.);
#885=FACE_OUTER_BOUND('',#1413,.T.);
#886=FACE_OUTER_BOUND('',#1414,.T.);
#887=FACE_OUTER_BOUND('',#1415,.T.);
#888=FACE_OUTER_BOUND('',#1416,.T.);
#889=FACE_OUTER_BOUND('',#1417,.T.);
#890=FACE_OUTER_BOUND('',#1418,.T.);
#891=FACE_OUTER_BOUND('',#1419,.T.);
#892=FACE_OUTER_BOUND('',#1420,.T.);
#893=FACE_OUTER_BOUND('',#1421,.T.);
#894=FACE_OUTER_BOUND('',#1422,.T.);
#895=FACE_OUTER_BOUND('',#1423,.T.);
#896=FACE_OUTER_BOUND('',#1424,.T.);
#897=FACE_OUTER_BOUND('',#1425,.T.);
#898=FACE_OUTER_BOUND('',#1427,.T.);
#899=FACE_OUTER_BOUND('',#1428,.T.);
#900=FACE_OUTER_BOUND('',#1430,.T.);
#1391=EDGE_LOOP('',(#7551,#7552,#7553,#7554));
#1392=EDGE_LOOP('',(#7555,#7556,#7557,#7558));
#1393=EDGE_LOOP('',(#7559,#7560,#7561,#7562));
#1394=EDGE_LOOP('',(#7563,#7564,#7565,#7566));
#1395=EDGE_LOOP('',(#7567,#7568,#7569,#7570));
#1396=EDGE_LOOP('',(#7571,#7572,#7573,#7574));
#1397=EDGE_LOOP('',(#7575,#7576,#7577,#7578));
#1398=EDGE_LOOP('',(#7579,#7580,#7581,#7582));
#1399=EDGE_LOOP('',(#7583,#7584,#7585,#7586));
#1400=EDGE_LOOP('',(#7587,#7588,#7589,#7590));
#1401=EDGE_LOOP('',(#7591,#7592,#7593,#7594));
#1402=EDGE_LOOP('',(#7595,#7596,#7597,#7598));
#1403=EDGE_LOOP('',(#7599,#7600,#7601,#7602));
#1404=EDGE_LOOP('',(#7603,#7604,#7605,#7606));
#1405=EDGE_LOOP('',(#7607,#7608,#7609,#7610));
#1406=EDGE_LOOP('',(#7611,#7612,#7613,#7614));
#1407=EDGE_LOOP('',(#7615,#7616,#7617,#7618));
#1408=EDGE_LOOP('',(#7619,#7620,#7621,#7622));
#1409=EDGE_LOOP('',(#7623,#7624,#7625,#7626));
#1410=EDGE_LOOP('',(#7627,#7628,#7629,#7630));
#1411=EDGE_LOOP('',(#7631,#7632,#7633,#7634));
#1412=EDGE_LOOP('',(#7635,#7636,#7637,#7638));
#1413=EDGE_LOOP('',(#7639,#7640,#7641,#7642,#7643,#7644,#7645,#7646));
#1414=EDGE_LOOP('',(#7647,#7648,#7649,#7650,#7651,#7652,#7653,#7654,#7655,
#7656,#7657,#7658,#7659,#7660,#7661,#7662,#7663,#7664,#7665,#7666,#7667,
#7668,#7669,#7670,#7671,#7672));
#1415=EDGE_LOOP('',(#7673,#7674,#7675,#7676));
#1416=EDGE_LOOP('',(#7677,#7678,#7679,#7680,#7681,#7682,#7683,#7684,#7685,
#7686,#7687,#7688,#7689,#7690,#7691,#7692,#7693,#7694,#7695,#7696,#7697,
#7698,#7699,#7700,#7701,#7702,#7703));
#1417=EDGE_LOOP('',(#7704,#7705,#7706,#7707));
#1418=EDGE_LOOP('',(#7708,#7709,#7710,#7711));
#1419=EDGE_LOOP('',(#7712,#7713,#7714,#7715));
#1420=EDGE_LOOP('',(#7716,#7717,#7718,#7719));
#1421=EDGE_LOOP('',(#7720,#7721,#7722,#7723));
#1422=EDGE_LOOP('',(#7724,#7725,#7726,#7727));
#1423=EDGE_LOOP('',(#7728,#7729,#7730,#7731));
#1424=EDGE_LOOP('',(#7732,#7733,#7734,#7735,#7736,#7737));
#1425=EDGE_LOOP('',(#7738));
#1426=EDGE_LOOP('',(#7739,#7740,#7741,#7742));
#1427=EDGE_LOOP('',(#7743,#7744,#7745,#7746));
#1428=EDGE_LOOP('',(#7747));
#1429=EDGE_LOOP('',(#7748,#7749,#7750,#7751,#7752,#7753));
#1430=EDGE_LOOP('',(#7754));
#1570=CIRCLE('',#9416,2.942);
#1571=CIRCLE('',#9428,2.37175);
#1572=CIRCLE('',#9440,2.942);
#1573=CIRCLE('',#9441,2.);
#1574=CIRCLE('',#9443,2.37175);
#1575=CIRCLE('',#9453,5.);
#1576=CIRCLE('',#9455,5.);
#2094=B_SPLINE_CURVE_WITH_KNOTS('',3,(#29424,#29425,#29426,#29427,#29428,
#29429,#29430,#29431,#29432,#29433),.UNSPECIFIED.,.F.,.F.,(4,3,3,4),(-4.09293042013066,
-3.9493215972006,-2.96199119790045,-2.06863817490914),.UNSPECIFIED.);
#2095=B_SPLINE_CURVE_WITH_KNOTS('',3,(#29436,#29437,#29438,#29439,#29440,
#29441,#29442),.UNSPECIFIED.,.F.,.F.,(4,3,4),(0.,0.988566943725272,1.11730040836823),
 .UNSPECIFIED.);
#2096=B_SPLINE_CURVE_WITH_KNOTS('',3,(#29447,#29448,#29449,#29450,#29451,
#29452,#29453,#29454,#29455,#29456,#29457,#29458,#29459,#29460,#29461,#29462,
#29463,#29464,#29465,#29466,#29467,#29468),.UNSPECIFIED.,.F.,.F.,(4,3,3,
3,3,3,3,4),(-10.3761157273102,-9.87330399300149,-8.88597359370134,-7.89864319440119,
-6.91131279510104,-5.92398239580089,-4.93665199650074,-4.09293042013066),
 .UNSPECIFIED.);
#2097=B_SPLINE_CURVE_WITH_KNOTS('',3,(#29469,#29470,#29471,#29472,#29473,
#29474,#29475,#29476,#29477,#29478,#29479,#29480,#29481,#29482,#29483,#29484,
#29485,#29486,#29487,#29488,#29489,#29490),.UNSPECIFIED.,.F.,.F.,(4,3,3,
3,3,3,3,4),(1.11730040836823,1.97713388745054,2.9657008311758,3.95426777490106,
4.94283471862632,5.93140166235159,6.91996860607685,7.40048571554782),
 .UNSPECIFIED.);
#2098=B_SPLINE_CURVE_WITH_KNOTS('',3,(#29495,#29496,#29497,#29498,#29499,
#29500,#29501,#29502,#29503,#29504,#29505,#29506,#29507,#29508,#29509,#29510,
#29511,#29512,#29513,#29514,#29515,#29516),.UNSPECIFIED.,.F.,.F.,(4,3,3,
3,3,3,3,4),(-16.6593010344898,-15.7972863888024,-14.8099559895022,-13.8226255902021,
-12.8352951909019,-11.8479647916018,-10.8606343923016,-10.3761157273102),
 .UNSPECIFIED.);
#2099=B_SPLINE_CURVE_WITH_KNOTS('',3,(#29517,#29518,#29519,#29520,#29521,
#29522,#29523,#29524,#29525,#29526,#29527,#29528,#29529,#29530,#29531,#29532,
#29533,#29534,#29535,#29536,#29537,#29538),.UNSPECIFIED.,.F.,.F.,(4,3,3,
3,3,3,3,4),(7.40048571554782,7.90853554980211,8.89710249352738,9.88566943725264,
10.8742363809779,11.8628033247032,12.8513702684284,13.6836710227274),
 .UNSPECIFIED.);
#2100=B_SPLINE_CURVE_WITH_KNOTS('',3,(#29543,#29544,#29545,#29546,#29547,
#29548,#29549,#29550,#29551,#29552,#29553,#29554,#29555,#29556,#29557,#29558,
#29559,#29560,#29561,#29562,#29563,#29564,#29565,#29566,#29567),
 .UNSPECIFIED.,.F.,.F.,(4,3,3,3,3,3,3,3,4),(-22.9424863416694,-22.7085991839034,
-21.7212687846033,-20.7339383853031,-19.746607986003,-18.7592775867028,
-17.7719471874027,-16.7846167881025,-16.6593010344898),.UNSPECIFIED.);
#2101=B_SPLINE_CURVE_WITH_KNOTS('',3,(#29568,#29569,#29570,#29571,#29572,
#29573,#29574,#29575,#29576,#29577,#29578,#29579,#29580,#29581,#29582,#29583,
#29584,#29585,#29586,#29587,#29588,#29589,#29590,#29591,#29592),
 .UNSPECIFIED.,.F.,.F.,(4,3,3,3,3,3,3,3,4),(13.6836710227274,13.8399372121537,
14.828504155879,15.8170710996042,16.8056380433295,17.7942049870548,18.78277193078,
19.7713388745053,19.966856329907),.UNSPECIFIED.);
#2102=B_SPLINE_CURVE_WITH_KNOTS('',3,(#29597,#29598,#29599,#29600,#29601,
#29602,#29603,#29604,#29605,#29606,#29607,#29608,#29609,#29610,#29611,#29612,
#29613,#29614,#29615,#29616,#29617,#29618),.UNSPECIFIED.,.F.,.F.,(4,3,3,
3,3,3,3,4),(-29.225671648849,-28.6325815797043,-27.6452511804042,-26.657920781104,
-25.6705903818039,-24.6832599825037,-23.6959295832036,-22.9424863416694),
 .UNSPECIFIED.);
#2103=B_SPLINE_CURVE_WITH_KNOTS('',3,(#29619,#29620,#29621,#29622,#29623,
#29624,#29625,#29626,#29627,#29628,#29629,#29630,#29631,#29632,#29633,#29634,
#29635,#29636,#29637,#29638,#29639,#29640),.UNSPECIFIED.,.F.,.F.,(4,3,3,
3,3,3,3,4),(19.966856329907,20.7599058182306,21.7484727619558,22.7370397056811,
23.7256066494064,24.7141735931316,25.7027405368569,26.2500416370866),
 .UNSPECIFIED.);
#2104=B_SPLINE_CURVE_WITH_KNOTS('',3,(#29645,#29646,#29647,#29648,#29649,
#29650,#29651,#29652,#29653,#29654,#29655,#29656,#29657,#29658,#29659,#29660,
#29661,#29662,#29663,#29664,#29665,#29666),.UNSPECIFIED.,.F.,.F.,(4,3,3,
3,3,3,3,4),(-35.5088569560286,-34.5565639755052,-33.5692335762051,-32.5819031769049,
-31.5945727776048,-30.6072423783046,-29.6199119790045,-29.225671648849),
 .UNSPECIFIED.);
#2105=B_SPLINE_CURVE_WITH_KNOTS('',3,(#29667,#29668,#29669,#29670,#29671,
#29672,#29673,#29674,#29675,#29676,#29677,#29678,#29679,#29680,#29681,#29682,
#29683,#29684,#29685,#29686,#29687,#29688),.UNSPECIFIED.,.F.,.F.,(4,3,3,
3,3,3,3,4),(26.2500416370866,26.6913074805822,27.6798744243074,28.6684413680327,
29.6570083117579,30.6455752554832,31.6341421992085,32.5332269442662),
 .UNSPECIFIED.);
#2106=B_SPLINE_CURVE_WITH_KNOTS('',3,(#29693,#29694,#29695,#29696,#29697,
#29698,#29699,#29700,#29701,#29702,#29703,#29704,#29705,#29706,#29707,#29708,
#29709,#29710,#29711,#29712,#29713,#29714,#29715,#29716,#29717),
 .UNSPECIFIED.,.F.,.F.,(4,3,3,3,3,3,3,3,4),(-41.7920422632082,-41.4678767706063,
-40.4805463713061,-39.4932159720059,-38.5058855727058,-37.5185551734057,
-36.5312247741055,-35.5438943748054,-35.5088569560286),.UNSPECIFIED.);
#2107=B_SPLINE_CURVE_WITH_KNOTS('',3,(#29718,#29719,#29720,#29721,#29722,
#29723,#29724,#29725,#29726,#29727,#29728,#29729,#29730,#29731,#29732,#29733,
#29734,#29735,#29736,#29737,#29738,#29739,#29740,#29741,#29742),
 .UNSPECIFIED.,.F.,.F.,(4,3,3,3,3,3,3,3,4),(32.5332269442662,32.6227091429337,
33.611276086659,34.5998430303843,35.5884099741095,36.5769769178348,37.5655438615601,
38.5541108052853,38.8164122514458),.UNSPECIFIED.);
#2108=B_SPLINE_CURVE_WITH_KNOTS('',3,(#29747,#29748,#29749,#29750,#29751,
#29752,#29753,#29754,#29755,#29756,#29757,#29758,#29759,#29760,#29761,#29762,
#29763,#29764,#29765,#29766,#29767,#29768),.UNSPECIFIED.,.F.,.F.,(4,3,3,
3,3,3,3,4),(-48.0752275703878,-47.3918591664071,-46.404528767107,-45.4171983678069,
-44.4298679685067,-43.4425375692066,-42.4552071699064,-41.7920422632082),
 .UNSPECIFIED.);
#2109=B_SPLINE_CURVE_WITH_KNOTS('',3,(#29769,#29770,#29771,#29772,#29773,
#29774,#29775,#29776,#29777,#29778,#29779,#29780,#29781,#29782,#29783,#29784,
#29785,#29786,#29787,#29788,#29789,#29790),.UNSPECIFIED.,.F.,.F.,(4,3,3,
3,3,3,3,4),(38.8164122514458,39.5426777490106,40.5312446927359,41.5198116364611,
42.5083785801864,43.4969455239117,44.4855124676369,45.0995975586253),
 .UNSPECIFIED.);
#2110=B_SPLINE_CURVE_WITH_KNOTS('',3,(#29795,#29796,#29797,#29798,#29799,
#29800,#29801,#29802,#29803,#29804,#29805,#29806,#29807,#29808,#29809,#29810,
#29811,#29812,#29813,#29814,#29815,#29816,#29817,#29818,#29819),
 .UNSPECIFIED.,.F.,.F.,(4,3,3,3,3,3,3,3,4),(-54.3584128775674,-54.3031719615082,
-53.315841562208,-52.3285111629079,-51.3411807636077,-50.3538503643076,
-49.3665199650074,-48.3791895657073,-48.0752275703878),.UNSPECIFIED.);
#2111=B_SPLINE_CURVE_WITH_KNOTS('',3,(#29820,#29821,#29822,#29823,#29824,
#29825,#29826,#29827,#29828,#29829,#29830,#29831,#29832,#29833,#29834,#29835,
#29836,#29837,#29838,#29839,#29840,#29841),.UNSPECIFIED.,.F.,.F.,(4,3,3,
3,3,3,3,4),(45.0995975586253,45.4740794113622,46.4626463550875,47.4512132988127,
48.439780242538,49.4283471862633,50.4169141299885,51.3827828658049),
 .UNSPECIFIED.);
#2112=B_SPLINE_CURVE_WITH_KNOTS('',3,(#29846,#29847,#29848,#29849,#29850,
#29851,#29852,#29853,#29854,#29855,#29856,#29857,#29858,#29859,#29860,#29861,
#29862,#29863,#29864,#29865,#29866,#29867),.UNSPECIFIED.,.F.,.F.,(4,3,3,
3,3,3,3,4),(-60.641598184747,-60.2271543573091,-59.2398239580089,-58.2524935587088,
-57.2651631594086,-56.2778327601085,-55.2905023608083,-54.3584128775674),
 .UNSPECIFIED.);
#2113=B_SPLINE_CURVE_WITH_KNOTS('',3,(#29868,#29869,#29870,#29871,#29872,
#29873,#29874,#29875,#29876,#29877,#29878,#29879,#29880,#29881,#29882,#29883,
#29884,#29885,#29886,#29887,#29888,#29889,#29890,#29891,#29892),
 .UNSPECIFIED.,.F.,.F.,(4,3,3,3,3,3,3,3,4),(51.3827828658049,51.4054810737138,
52.394048017439,53.3826149611643,54.3711819048896,55.3597488486148,56.3483157923401,
57.3368827360654,57.6659681729845),.UNSPECIFIED.);
#2114=B_SPLINE_CURVE_WITH_KNOTS('',3,(#29897,#29898,#29899,#29900,#29901,
#29902,#29903,#29904,#29905,#29906,#29907,#29908,#29909,#29910,#29911,#29912,
#29913,#29914,#29915,#29916,#29917,#29918),.UNSPECIFIED.,.F.,.F.,(4,3,3,
3,3,3,3,4),(-66.9247834919266,-66.15113675311,-65.1638063538098,-64.1764759545097,
-63.1891455552095,-62.2018151559094,-61.2144847566092,-60.641598184747),
 .UNSPECIFIED.);
#2115=B_SPLINE_CURVE_WITH_KNOTS('',3,(#29919,#29920,#29921,#29922,#29923,
#29924,#29925,#29926,#29927,#29928,#29929,#29930,#29931,#29932,#29933,#29934,
#29935,#29936,#29937,#29938,#29939,#29940),.UNSPECIFIED.,.F.,.F.,(4,3,3,
3,3,3,3,4),(57.6659681729845,58.3254496797906,59.3140166235159,60.3025835672412,
61.2911505109664,62.2797174546917,63.268284398417,63.9491534801641),
 .UNSPECIFIED.);
#2116=B_SPLINE_CURVE_WITH_KNOTS('',3,(#29946,#29947,#29948,#29949,#29950,
#29951,#29952,#29953,#29954,#29955),.UNSPECIFIED.,.F.,.F.,(4,1,1,1,1,1,
1,4),(78.5398163397448,78.7535000002284,79.7408303995285,80.7281607988287,
81.7154911981288,82.702821597429,83.6901519967291,84.6774823960293),
 .UNSPECIFIED.);
#2117=B_SPLINE_CURVE_WITH_KNOTS('',3,(#29958,#29959,#29960,#29961,#29962,
#29963,#29964,#29965),.UNSPECIFIED.,.F.,.F.,(4,1,1,1,1,4),(78.5398163397448,
79.4842975006201,80.4728644443454,81.4614313880706,82.4499983317959,83.4385652755212),
 .UNSPECIFIED.);
#2118=B_SPLINE_CURVE_WITH_KNOTS('',3,(#29970,#29971,#29972,#29973,#29974,
#29975,#29976,#29977,#29978,#29979),.UNSPECIFIED.,.F.,.F.,(4,1,1,1,1,1,
1,4),(72.2566310325653,72.8295176044275,73.8168480037276,74.8041784030278,
75.7915088023279,76.7788392016281,77.7661696009282,78.5398163397448),
 .UNSPECIFIED.);
#2119=B_SPLINE_CURVE_WITH_KNOTS('',3,(#29980,#29981,#29982,#29983,#29984,
#29985,#29986,#29987,#29988,#29989,#29990),.UNSPECIFIED.,.F.,.F.,(4,1,1,
1,1,1,1,1,4),(72.2566310325652,72.5643288945433,73.5528958382685,74.5414627819938,
75.530029725719,76.5185966694443,77.5071636131696,78.4957305568948,78.5398163397448),
 .UNSPECIFIED.);
#2120=B_SPLINE_CURVE_WITH_KNOTS('',3,(#29995,#29996,#29997,#29998,#29999,
#30000,#30001,#30002,#30003,#30004),.UNSPECIFIED.,.F.,.F.,(4,1,1,1,1,1,
1,4),(65.9734457253856,66.9055352086266,67.8928656079267,68.8801960072269,
69.867526406527,70.8548568058272,71.8421872051273,72.2566310325653),
 .UNSPECIFIED.);
#2121=B_SPLINE_CURVE_WITH_KNOTS('',3,(#30005,#30006,#30007,#30008,#30009,
#30010,#30011,#30012,#30013,#30014),.UNSPECIFIED.,.F.,.F.,(4,1,1,1,1,1,
1,4),(65.9734457253856,66.6329272321917,67.6214941759169,68.6100611196422,
69.5986280633675,70.5871950070927,71.575761950818,72.2566310325652),
 .UNSPECIFIED.);
#2122=B_SPLINE_CURVE_WITH_KNOTS('',3,(#30019,#30020,#30021,#30022,#30023,
#30024,#30025,#30026,#30027,#30028,#30029),.UNSPECIFIED.,.F.,.F.,(4,1,1,
1,1,1,1,1,4),(59.6902604182061,59.9942224135255,60.9815528128257,61.9688832121258,
62.956213611426,63.9435440107261,64.9308744100263,65.9182048093264,65.9734457253856),
 .UNSPECIFIED.);
#2123=B_SPLINE_CURVE_WITH_KNOTS('',3,(#30030,#30031,#30032,#30033,#30034,
#30035,#30036,#30037,#30038,#30039,#30040),.UNSPECIFIED.,.F.,.F.,(4,1,1,
1,1,1,1,1,4),(59.6902604182061,59.7129586261148,60.7015255698401,61.6900925135653,
62.6786594572906,63.6672264010159,64.6557933447411,65.6443602884664,65.9734457253856),
 .UNSPECIFIED.);
#2124=B_SPLINE_CURVE_WITH_KNOTS('',3,(#30045,#30046,#30047,#30048,#30049,
#30050,#30051,#30052,#30053,#30054),.UNSPECIFIED.,.F.,.F.,(4,1,1,1,1,1,
1,4),(53.4070751110265,54.0702400177247,55.0575704170248,56.0449008163249,
57.0322312156251,58.0195616149252,59.0068920142254,59.6902604182061),
 .UNSPECIFIED.);
#2125=B_SPLINE_CURVE_WITH_KNOTS('',3,(#30055,#30056,#30057,#30058,#30059,
#30060,#30061,#30062,#30063,#30064),.UNSPECIFIED.,.F.,.F.,(4,1,1,1,1,1,
1,4),(53.4070751110265,53.7815569637632,54.7701239074885,55.7586908512138,
56.747257794939,57.7358247386643,58.7243916823895,59.6902604182061),
 .UNSPECIFIED.);
#2126=B_SPLINE_CURVE_WITH_KNOTS('',3,(#30069,#30070,#30071,#30072,#30073,
#30074,#30075,#30076,#30077,#30078,#30079),.UNSPECIFIED.,.F.,.F.,(4,1,1,
1,1,1,1,1,4),(47.1238898038469,47.1589272226236,48.1462576219238,49.1335880212239,
50.1209184205241,51.1082488198242,52.0955792191244,53.0829096184245,53.4070751110265),
 .UNSPECIFIED.);
#2127=B_SPLINE_CURVE_WITH_KNOTS('',3,(#30080,#30081,#30082,#30083,#30084,
#30085,#30086,#30087,#30088,#30089),.UNSPECIFIED.,.F.,.F.,(4,1,1,1,1,1,
1,4),(47.1238898038469,47.8501553014116,48.8387222451369,49.8272891888622,
50.8158561325874,51.8044230763127,52.792990020038,53.4070751110265),
 .UNSPECIFIED.);
#2128=B_SPLINE_CURVE_WITH_KNOTS('',3,(#30094,#30095,#30096,#30097,#30098,
#30099,#30100,#30101,#30102,#30103),.UNSPECIFIED.,.F.,.F.,(4,1,1,1,1,1,
1,4),(40.8407044966673,41.2349448268227,42.2222752261229,43.209605625423,
44.1969360247232,45.1842664240233,46.1715968233235,47.1238898038469),
 .UNSPECIFIED.);
#2129=B_SPLINE_CURVE_WITH_KNOTS('',3,(#30104,#30105,#30106,#30107,#30108,
#30109,#30110,#30111,#30112,#30113,#30114),.UNSPECIFIED.,.F.,.F.,(4,1,1,
1,1,1,1,1,4),(40.8407044966673,40.9301866953348,41.91875363906,42.9073205827853,
43.8958875265106,44.8844544702358,45.8730214139611,46.8615883576864,47.1238898038469),
 .UNSPECIFIED.);
#2130=B_SPLINE_CURVE_WITH_KNOTS('',3,(#30119,#30120,#30121,#30122,#30123,
#30124,#30125,#30126,#30127,#30128),.UNSPECIFIED.,.F.,.F.,(4,1,1,1,1,1,
1,4),(34.5575191894877,35.3109624310218,36.298292830322,37.2856232296221,
38.2729536289223,39.2602840282224,40.2476144275226,40.8407044966673),
 .UNSPECIFIED.);
#2131=B_SPLINE_CURVE_WITH_KNOTS('',3,(#30129,#30130,#30131,#30132,#30133,
#30134,#30135,#30136,#30137,#30138),.UNSPECIFIED.,.F.,.F.,(4,1,1,1,1,1,
1,4),(34.5575191894877,34.9987850329832,35.9873519767085,36.9759189204337,
37.964485864159,38.9530528078842,39.9416197516095,40.8407044966673),
 .UNSPECIFIED.);
#2132=B_SPLINE_CURVE_WITH_KNOTS('',3,(#30143,#30144,#30145,#30146,#30147,
#30148,#30149,#30150,#30151,#30152,#30153),.UNSPECIFIED.,.F.,.F.,(4,1,1,
1,1,1,1,1,4),(28.2743338823081,28.3996496359208,29.3869800352209,30.3743104345211,
31.3616408338212,32.3489712331214,33.3363016324215,34.3236320317217,34.5575191894877),
 .UNSPECIFIED.);
#2133=B_SPLINE_CURVE_WITH_KNOTS('',3,(#30154,#30155,#30156,#30157,#30158,
#30159,#30160,#30161,#30162,#30163),.UNSPECIFIED.,.F.,.F.,(4,1,1,1,1,1,
1,4),(28.2743338823081,29.0673833706316,30.0559503143569,31.0445172580821,
32.0330842018074,33.0216511455327,34.0102180892579,34.5575191894877),
 .UNSPECIFIED.);
#2134=B_SPLINE_CURVE_WITH_KNOTS('',3,(#30168,#30169,#30170,#30171,#30172,
#30173,#30174,#30175,#30176,#30177),.UNSPECIFIED.,.F.,.F.,(4,1,1,1,1,1,
1,4),(21.9911485751285,22.4756672401199,23.46299763942,24.4503280387202,
25.4376584380203,26.4249888373205,27.4123192366206,28.2743338823081),
 .UNSPECIFIED.);
#2135=B_SPLINE_CURVE_WITH_KNOTS('',3,(#30178,#30179,#30180,#30181,#30182,
#30183,#30184,#30185,#30186,#30187,#30188),.UNSPECIFIED.,.F.,.F.,(4,1,1,
1,1,1,1,1,4),(21.9911485751285,22.1474147645547,23.13598170828,24.1245486520053,
25.1131155957305,26.1016825394558,27.0902494831811,28.0788164269063,28.2743338823081),
 .UNSPECIFIED.);
#2136=B_SPLINE_CURVE_WITH_KNOTS('',3,(#30193,#30194,#30195,#30196,#30197,
#30198,#30199,#30200,#30201,#30202),.UNSPECIFIED.,.F.,.F.,(4,1,1,1,1,1,
1,4),(15.7079632679489,16.551684844319,17.5390152436191,18.5263456429193,
19.5136760422194,20.5010064415196,21.4883368408197,21.9911485751285),
 .UNSPECIFIED.);
#2137=B_SPLINE_CURVE_WITH_KNOTS('',3,(#30203,#30204,#30205,#30206,#30207,
#30208,#30209,#30210,#30211,#30212),.UNSPECIFIED.,.F.,.F.,(4,1,1,1,1,1,
1,4),(15.7079632679489,16.2160131022032,17.2045800459284,18.1931469896537,
19.181713933379,20.1702808771042,21.1588478208295,21.9911485751285),
 .UNSPECIFIED.);
#2138=B_SPLINE_CURVE_WITH_KNOTS('',3,(#30215,#30216,#30217,#30218,#30219,
#30220,#30221,#30222,#30223,#30224,#30225,#30226,#30227,#30228,#30229,#30230,
#30231,#30232,#30233,#30234,#30235,#30236,#30237,#30238,#30239,#30240,#30241,
#30242,#30243,#30244,#30245,#30246,#30247,#30248,#30249,#30250,#30251,#30252,
#30253,#30254,#30255,#30256,#30257,#30258,#30259,#30260,#30261,#30262,#30263,
#30264,#30265,#30266,#30267,#30268,#30269,#30270,#30271,#30272,#30273,#30274,
#30275,#30276,#30277,#30278,#30279,#30280,#30281,#30282,#30283,#30284,#30285,
#30286,#30287,#30288,#30289,#30290,#30291,#30292,#30293,#30294,#30295,#30296,
#30297,#30298,#30299,#30300,#30301,#30302,#30303,#30304,#30305,#30306,#30307,
#30308,#30309,#30310,#30311,#30312,#30313,#30314,#30315,#30316,#30317,#30318,
#30319,#30320,#30321,#30322,#30323,#30324,#30325,#30326,#30327,#30328,#30329,
#30330,#30331,#30332,#30333,#30334,#30335,#30336,#30337,#30338,#30339,#30340,
#30341,#30342,#30343,#30344,#30345,#30346,#30347,#30348,#30349,#30350,#30351,
#30352,#30353,#30354,#30355,#30356,#30357,#30358,#30359,#30360,#30361,#30362,
#30363,#30364,#30365,#30366,#30367,#30368,#30369,#30370,#30371,#30372,#30373,
#30374,#30375,#30376,#30377,#30378,#30379,#30380,#30381,#30382,#30383,#30384,
#30385,#30386,#30387,#30388,#30389,#30390,#30391,#30392,#30393,#30394,#30395,
#30396,#30397,#30398,#30399,#30400,#30401,#30402,#30403,#30404,#30405,#30406,
#30407,#30408,#30409,#30410,#30411,#30412,#30413,#30414,#30415,#30416,#30417,
#30418,#30419,#30420,#30421,#30422,#30423,#30424,#30425,#30426,#30427,#30428,
#30429,#30430,#30431),.UNSPECIFIED.,.F.,.F.,(4,3,3,3,3,3,3,3,3,3,3,3,3,
3,3,3,3,3,3,3,3,3,3,3,3,3,3,3,3,3,3,3,3,3,3,3,3,3,3,3,3,3,3,3,3,3,3,3,3,
3,3,3,3,3,3,3,3,3,3,3,3,3,3,3,3,3,3,3,3,3,3,3,4),(-1.51155304937228,-1.48679174718013,
-1.46137597198077,-1.44942691521821,-1.44205848651244,-1.43724119559823,
-1.41130764113729,-1.38514768961224,-1.36936593028954,-1.36512230166791,
-1.33867581137855,-1.31235917608035,-1.29127511993008,-1.28073309185494,
-1.2739086628828,-1.27019106377981,-1.24488979836553,-1.21884130205047,
-1.19384888620637,-1.18291470427457,-1.17641188206357,-1.17130697868968,
-1.14451640582175,-1.11742561305122,-1.09279470361283,-1.08177565945417,
-1.07670730294613,-1.07245364414871,-1.0452101587782,-1.01890197529764,
-0.992076665792053,-0.977095538498891,-0.971310437727824,-0.944262984582137,
-0.91671696123902,-0.889051349044572,-0.8786107219546,-0.873404326505122,
-0.869185758667877,-0.841205731090746,-0.813331817877821,-0.785648584359967,
-0.771436006282574,-0.765308450445371,-0.757965350842113,-0.731019445974318,
-0.703340715547858,-0.676331238706378,-0.668063308133434,-0.663247880961674,
-0.658967945513649,-0.630690110839631,-0.602089962339152,-0.573383696958367,
-0.562618847440572,-0.556352694911719,-0.55203012393032,-0.523164492059728,
-0.494713544949419,-0.487264900816012,-0.45884309987075,-0.449622389577847,
-0.445165938771905,-0.416742684601646,-0.387755299334011,-0.358563756837841,
-0.34211828207705,-0.337697582134308,-0.308241853281341,-0.278784672736061,
-0.25000255453776,-0.226999958751515,-0.219677966288006),.UNSPECIFIED.);
#2139=B_SPLINE_CURVE_WITH_KNOTS('',3,(#30433,#30434,#30435,#30436,#30437,
#30438,#30439,#30440,#30441,#30442,#30443,#30444,#30445,#30446,#30447,#30448,
#30449,#30450,#30451,#30452,#30453,#30454,#30455,#30456,#30457,#30458,#30459,
#30460,#30461,#30462,#30463,#30464,#30465,#30466,#30467,#30468,#30469,#30470,
#30471,#30472,#30473,#30474,#30475,#30476,#30477,#30478,#30479,#30480,#30481,
#30482,#30483,#30484,#30485,#30486,#30487,#30488,#30489,#30490,#30491,#30492,
#30493),.UNSPECIFIED.,.F.,.F.,(4,3,3,3,3,3,3,3,3,3,3,3,3,3,3,3,3,3,3,3,
4),(-0.410648750432938,-0.381294613665594,-0.352267124576947,-0.328792823836752,
-0.311187098281605,-0.306018425011984,-0.301691296836585,-0.274143229574461,
-0.258369921616165,-0.230117472373342,-0.201352788326674,-0.195525900786732,
-0.16833922287309,-0.141249160586392,-0.114615533759621,-0.100282139063474,
-0.0960342097686789,-0.0702554174629941,-0.0448546715641945,-0.0201984500449382,
0.),.UNSPECIFIED.);
#2140=B_SPLINE_CURVE_WITH_KNOTS('',3,(#30496,#30497,#30498,#30499,#30500,
#30501,#30502,#30503,#30504,#30505,#30506,#30507,#30508,#30509,#30510,#30511,
#30512,#30513,#30514,#30515,#30516,#30517,#30518,#30519,#30520,#30521,#30522,
#30523,#30524,#30525,#30526),.UNSPECIFIED.,.F.,.F.,(4,3,3,3,3,3,3,3,3,3,
4),(-0.219677966288006,-0.206985183547511,-0.178213580556878,-0.148819200354015,
-0.130216800309763,-0.118450459252591,-0.113866160083042,-0.0841488051349767,
-0.0540951018364117,-0.0242019686830237,0.),.UNSPECIFIED.);
#2141=B_SPLINE_CURVE_WITH_KNOTS('',3,(#30839,#30840,#30841,#30842,#30843,
#30844,#30845,#30846),.UNSPECIFIED.,.F.,.F.,(4,1,1,1,1,4),(11.6150328478182,
12.6023632471184,13.5896936464185,14.5770240457187,15.5643544450188,15.7079632679489),
 .UNSPECIFIED.);
#2142=B_SPLINE_CURVE_WITH_KNOTS('',3,(#30847,#30848,#30849,#30850,#30851,
#30852,#30853,#30854,#30855,#30856,#30857,#30858,#30859,#30860,#30861,#30862,
#30863,#30864,#30865,#30866,#30867,#30868,#30869,#30870,#30871,#30872,#30873,
#30874,#30875,#30876,#30877,#30878,#30879,#30880,#30881,#30882,#30883,#30884,
#30885,#30886,#30887,#30888,#30889,#30890,#30891,#30892,#30893,#30894,#30895,
#30896,#30897,#30898,#30899,#30900,#30901,#30902,#30903,#30904,#30905,#30906,
#30907,#30908,#30909,#30910,#30911,#30912,#30913,#30914,#30915,#30916,#30917,
#30918,#30919,#30920,#30921,#30922,#30923,#30924,#30925,#30926,#30927,#30928,
#30929,#30930,#30931,#30932,#30933,#30934),.UNSPECIFIED.,.F.,.F.,(4,3,3,
3,3,3,3,3,3,3,3,3,3,3,3,3,3,3,3,3,3,3,3,3,3,3,3,3,3,4),(-0.55274537837504,
-0.525174630400016,-0.495740003900857,-0.479498227927527,-0.472105972866577,
-0.443064611280178,-0.418881458903182,-0.408301329738247,-0.401969450637142,
-0.397429868442983,-0.369124488132221,-0.341064938672273,-0.313899750226951,
-0.29772704364586,-0.291366968188088,-0.264559598151202,-0.249599392264211,
-0.222215347947115,-0.194438429453726,-0.189292991414398,-0.162670593649827,
-0.136062352557756,-0.109859916217256,-0.101879142728474,-0.0950850259724172,
-0.09115324392662,-0.0655931049079899,-0.0404250325776628,-0.0160423336449029,
0.),.UNSPECIFIED.);
#2143=B_SPLINE_CURVE_WITH_KNOTS('',3,(#30935,#30936,#30937,#30938,#30939,
#30940,#30941,#30942,#30943,#30944,#30945,#30946,#30947,#30948,#30949,#30950,
#30951,#30952,#30953),.UNSPECIFIED.,.F.,.F.,(4,3,3,3,3,3,4),(-71.548101301701,
-71.0877887496107,-70.1004583503106,-69.1131279510104,-68.1257975517103,
-67.1384671524101,-66.9247834919266),.UNSPECIFIED.);
#2144=B_SPLINE_CURVE_WITH_KNOTS('',3,(#30956,#30957,#30958,#30959,#30960,
#30961,#30962,#30963,#30964),.UNSPECIFIED.,.F.,.F.,(4,1,1,1,1,1,4),(10.3761157273102,
11.2731783835768,12.2617453273021,13.2503122710274,14.2388792147526,15.2274461584779,
15.7079632679489),.UNSPECIFIED.);
#2145=B_SPLINE_CURVE_WITH_KNOTS('',3,(#31282,#31283,#31284,#31285,#31286,
#31287,#31288,#31289,#31290,#31291,#31292,#31293,#31294,#31295,#31296,#31297,
#31298,#31299,#31300,#31301,#31302,#31303),.UNSPECIFIED.,.F.,.F.,(4,3,3,
3,3,3,3,4),(63.9491534801641,64.2568513421422,65.2454182858675,66.2339852295928,
67.222552173318,68.2111191170433,69.1996860607685,69.4794631267919),
 .UNSPECIFIED.);
#2146=B_SPLINE_CURVE_WITH_KNOTS('',3,(#31304,#31305,#31306,#31307,#31308,
#31309,#31310,#31311,#31312,#31313,#31314,#31315,#31316,#31317,#31318,#31319,
#31320,#31321,#31322,#31323,#31324,#31325,#31326,#31327,#31328,#31329,#31330,
#31331,#31332,#31333,#31334,#31335,#31336,#31337,#31338,#31339,#31340,#31341,
#31342,#31343,#31344,#31345,#31346,#31347,#31348,#31349,#31350,#31351,#31352,
#31353,#31354,#31355,#31356,#31357,#31358,#31359,#31360,#31361,#31362,#31363,
#31364,#31365,#31366,#31367,#31368,#31369,#31370,#31371,#31372,#31373,#31374,
#31375,#31376,#31377,#31378,#31379,#31380,#31381,#31382,#31383,#31384,#31385,
#31386,#31387,#31388,#31389,#31390,#31391),.UNSPECIFIED.,.F.,.F.,(4,3,3,
3,3,3,3,3,3,3,3,3,3,3,3,3,3,3,3,3,3,3,3,3,3,3,3,3,3,4),(-0.555272788399385,
-0.533197712400843,-0.50841200558917,-0.492097097422296,-0.487698425831477,
-0.461722637175749,-0.438993822101987,-0.427671428401512,-0.42202191869945,
-0.395458071621424,-0.368431943977533,-0.346296987129563,-0.329695769493585,
-0.32517826205158,-0.321068892319616,-0.293156561268766,-0.279892116585652,
-0.25291117159626,-0.225403496298925,-0.221057334466692,-0.216708298034074,
-0.188764735094145,-0.160284152968102,-0.131561788206246,-0.114355289595352,
-0.109564750157472,-0.0800994390258527,-0.050557237845911,-0.0215776241374192,
0.),.UNSPECIFIED.);
#2649=LINE('',#29422,#3195);
#2650=LINE('',#29446,#3196);
#2651=LINE('',#29494,#3197);
#2652=LINE('',#29542,#3198);
#2653=LINE('',#29596,#3199);
#2654=LINE('',#29644,#3200);
#2655=LINE('',#29692,#3201);
#2656=LINE('',#29746,#3202);
#2657=LINE('',#29794,#3203);
#2658=LINE('',#29845,#3204);
#2659=LINE('',#29896,#3205);
#2660=LINE('',#29944,#3206);
#2661=LINE('',#29969,#3207);
#2662=LINE('',#29994,#3208);
#2663=LINE('',#30018,#3209);
#2664=LINE('',#30044,#3210);
#2665=LINE('',#30068,#3211);
#2666=LINE('',#30093,#3212);
#2667=LINE('',#30118,#3213);
#2668=LINE('',#30142,#3214);
#2669=LINE('',#30167,#3215);
#2670=LINE('',#30192,#3216);
#2671=LINE('',#30528,#3217);
#2672=LINE('',#31396,#3218);
#2673=LINE('',#31398,#3219);
#2674=LINE('',#31400,#3220);
#2675=LINE('',#31401,#3221);
#2676=LINE('',#31404,#3222);
#2677=LINE('',#31406,#3223);
#2678=LINE('',#31407,#3224);
#2679=LINE('',#31410,#3225);
#2680=LINE('',#31412,#3226);
#2681=LINE('',#31413,#3227);
#2682=LINE('',#31416,#3228);
#2683=LINE('',#31418,#3229);
#2684=LINE('',#31419,#3230);
#2685=LINE('',#31422,#3231);
#2686=LINE('',#31424,#3232);
#2687=LINE('',#31425,#3233);
#2688=LINE('',#31427,#3234);
#2689=LINE('',#31428,#3235);
#2690=LINE('',#31435,#3236);
#3195=VECTOR('',#11051,3.);
#3196=VECTOR('',#11056,3.);
#3197=VECTOR('',#11059,3.);
#3198=VECTOR('',#11062,3.);
#3199=VECTOR('',#11065,3.);
#3200=VECTOR('',#11068,3.);
#3201=VECTOR('',#11071,3.);
#3202=VECTOR('',#11074,3.);
#3203=VECTOR('',#11077,3.);
#3204=VECTOR('',#11080,3.);
#3205=VECTOR('',#11083,3.);
#3206=VECTOR('',#11086,2.37175);
#3207=VECTOR('',#11091,2.37175);
#3208=VECTOR('',#11094,2.37175);
#3209=VECTOR('',#11097,2.37175);
#3210=VECTOR('',#11100,2.37175);
#3211=VECTOR('',#11103,2.37175);
#3212=VECTOR('',#11106,2.37175);
#3213=VECTOR('',#11109,2.37175);
#3214=VECTOR('',#11112,2.37175);
#3215=VECTOR('',#11115,2.37175);
#3216=VECTOR('',#11118,2.37175);
#3217=VECTOR('',#11123,2.5);
#3218=VECTOR('',#11134,10.);
#3219=VECTOR('',#11135,10.);
#3220=VECTOR('',#11136,10.);
#3221=VECTOR('',#11137,10.);
#3222=VECTOR('',#11140,10.);
#3223=VECTOR('',#11141,10.);
#3224=VECTOR('',#11142,10.);
#3225=VECTOR('',#11145,10.);
#3226=VECTOR('',#11146,10.);
#3227=VECTOR('',#11147,10.);
#3228=VECTOR('',#11150,10.);
#3229=VECTOR('',#11151,10.);
#3230=VECTOR('',#11152,10.);
#3231=VECTOR('',#11155,10.);
#3232=VECTOR('',#11156,10.);
#3233=VECTOR('',#11157,10.);
#3234=VECTOR('',#11160,10.);
#3235=VECTOR('',#11161,10.);
#3236=VECTOR('',#11170,5.);
#3995=VERTEX_POINT('',#29420);
#3996=VERTEX_POINT('',#29421);
#3997=VERTEX_POINT('',#29423);
#3998=VERTEX_POINT('',#29434);
#3999=VERTEX_POINT('',#29444);
#4000=VERTEX_POINT('',#29445);
#4001=VERTEX_POINT('',#29492);
#4002=VERTEX_POINT('',#29493);
#4003=VERTEX_POINT('',#29540);
#4004=VERTEX_POINT('',#29541);
#4005=VERTEX_POINT('',#29594);
#4006=VERTEX_POINT('',#29595);
#4007=VERTEX_POINT('',#29642);
#4008=VERTEX_POINT('',#29643);
#4009=VERTEX_POINT('',#29690);
#4010=VERTEX_POINT('',#29691);
#4011=VERTEX_POINT('',#29744);
#4012=VERTEX_POINT('',#29745);
#4013=VERTEX_POINT('',#29792);
#4014=VERTEX_POINT('',#29793);
#4015=VERTEX_POINT('',#29843);
#4016=VERTEX_POINT('',#29844);
#4017=VERTEX_POINT('',#29894);
#4018=VERTEX_POINT('',#29895);
#4019=VERTEX_POINT('',#29942);
#4020=VERTEX_POINT('',#29943);
#4021=VERTEX_POINT('',#29945);
#4022=VERTEX_POINT('',#29956);
#4023=VERTEX_POINT('',#29967);
#4024=VERTEX_POINT('',#29968);
#4025=VERTEX_POINT('',#29992);
#4026=VERTEX_POINT('',#29993);
#4027=VERTEX_POINT('',#30016);
#4028=VERTEX_POINT('',#30017);
#4029=VERTEX_POINT('',#30042);
#4030=VERTEX_POINT('',#30043);
#4031=VERTEX_POINT('',#30066);
#4032=VERTEX_POINT('',#30067);
#4033=VERTEX_POINT('',#30091);
#4034=VERTEX_POINT('',#30092);
#4035=VERTEX_POINT('',#30116);
#4036=VERTEX_POINT('',#30117);
#4037=VERTEX_POINT('',#30140);
#4038=VERTEX_POINT('',#30141);
#4039=VERTEX_POINT('',#30165);
#4040=VERTEX_POINT('',#30166);
#4041=VERTEX_POINT('',#30190);
#4042=VERTEX_POINT('',#30191);
#4043=VERTEX_POINT('',#30214);
#4044=VERTEX_POINT('',#30432);
#4045=VERTEX_POINT('',#30494);
#4046=VERTEX_POINT('',#30527);
#4047=VERTEX_POINT('',#30838);
#4048=VERTEX_POINT('',#30955);
#4049=VERTEX_POINT('',#31394);
#4050=VERTEX_POINT('',#31395);
#4051=VERTEX_POINT('',#31397);
#4052=VERTEX_POINT('',#31399);
#4053=VERTEX_POINT('',#31403);
#4054=VERTEX_POINT('',#31405);
#4055=VERTEX_POINT('',#31409);
#4056=VERTEX_POINT('',#31411);
#4057=VERTEX_POINT('',#31415);
#4058=VERTEX_POINT('',#31417);
#4059=VERTEX_POINT('',#31421);
#4060=VERTEX_POINT('',#31423);
#4061=VERTEX_POINT('',#31431);
#4062=VERTEX_POINT('',#31434);
#5199=EDGE_CURVE('',#3995,#3996,#2649,.T.);
#5200=EDGE_CURVE('',#3995,#3997,#2094,.T.);
#5201=EDGE_CURVE('',#3997,#3998,#1570,.F.);
#5202=EDGE_CURVE('',#3998,#3996,#2095,.T.);
#5203=EDGE_CURVE('',#3999,#4000,#2650,.T.);
#5204=EDGE_CURVE('',#3999,#3995,#2096,.T.);
#5205=EDGE_CURVE('',#3996,#4000,#2097,.T.);
#5206=EDGE_CURVE('',#4001,#4002,#2651,.T.);
#5207=EDGE_CURVE('',#4001,#3999,#2098,.T.);
#5208=EDGE_CURVE('',#4000,#4002,#2099,.T.);
#5209=EDGE_CURVE('',#4003,#4004,#2652,.T.);
#5210=EDGE_CURVE('',#4003,#4001,#2100,.T.);
#5211=EDGE_CURVE('',#4002,#4004,#2101,.T.);
#5212=EDGE_CURVE('',#4005,#4006,#2653,.T.);
#5213=EDGE_CURVE('',#4005,#4003,#2102,.T.);
#5214=EDGE_CURVE('',#4004,#4006,#2103,.T.);
#5215=EDGE_CURVE('',#4007,#4008,#2654,.T.);
#5216=EDGE_CURVE('',#4007,#4005,#2104,.T.);
#5217=EDGE_CURVE('',#4006,#4008,#2105,.T.);
#5218=EDGE_CURVE('',#4009,#4010,#2655,.T.);
#5219=EDGE_CURVE('',#4009,#4007,#2106,.T.);
#5220=EDGE_CURVE('',#4008,#4010,#2107,.T.);
#5221=EDGE_CURVE('',#4011,#4012,#2656,.T.);
#5222=EDGE_CURVE('',#4011,#4009,#2108,.T.);
#5223=EDGE_CURVE('',#4010,#4012,#2109,.T.);
#5224=EDGE_CURVE('',#4013,#4014,#2657,.T.);
#5225=EDGE_CURVE('',#4013,#4011,#2110,.T.);
#5226=EDGE_CURVE('',#4012,#4014,#2111,.T.);
#5227=EDGE_CURVE('',#4015,#4016,#2658,.T.);
#5228=EDGE_CURVE('',#4015,#4013,#2112,.T.);
#5229=EDGE_CURVE('',#4014,#4016,#2113,.T.);
#5230=EDGE_CURVE('',#4017,#4018,#2659,.T.);
#5231=EDGE_CURVE('',#4017,#4015,#2114,.T.);
#5232=EDGE_CURVE('',#4016,#4018,#2115,.T.);
#5233=EDGE_CURVE('',#4019,#4020,#2660,.T.);
#5234=EDGE_CURVE('',#4019,#4021,#2116,.T.);
#5235=EDGE_CURVE('',#4021,#4022,#1571,.T.);
#5236=EDGE_CURVE('',#4020,#4022,#2117,.T.);
#5237=EDGE_CURVE('',#4023,#4024,#2661,.T.);
#5238=EDGE_CURVE('',#4023,#4019,#2118,.T.);
#5239=EDGE_CURVE('',#4024,#4020,#2119,.T.);
#5240=EDGE_CURVE('',#4025,#4026,#2662,.T.);
#5241=EDGE_CURVE('',#4025,#4023,#2120,.T.);
#5242=EDGE_CURVE('',#4026,#4024,#2121,.T.);
#5243=EDGE_CURVE('',#4027,#4028,#2663,.T.);
#5244=EDGE_CURVE('',#4027,#4025,#2122,.T.);
#5245=EDGE_CURVE('',#4028,#4026,#2123,.T.);
#5246=EDGE_CURVE('',#4029,#4030,#2664,.T.);
#5247=EDGE_CURVE('',#4029,#4027,#2124,.T.);
#5248=EDGE_CURVE('',#4030,#4028,#2125,.T.);
#5249=EDGE_CURVE('',#4031,#4032,#2665,.T.);
#5250=EDGE_CURVE('',#4031,#4029,#2126,.T.);
#5251=EDGE_CURVE('',#4032,#4030,#2127,.T.);
#5252=EDGE_CURVE('',#4033,#4034,#2666,.T.);
#5253=EDGE_CURVE('',#4033,#4031,#2128,.T.);
#5254=EDGE_CURVE('',#4034,#4032,#2129,.T.);
#5255=EDGE_CURVE('',#4035,#4036,#2667,.T.);
#5256=EDGE_CURVE('',#4035,#4033,#2130,.T.);
#5257=EDGE_CURVE('',#4036,#4034,#2131,.T.);
#5258=EDGE_CURVE('',#4037,#4038,#2668,.T.);
#5259=EDGE_CURVE('',#4037,#4035,#2132,.T.);
#5260=EDGE_CURVE('',#4038,#4036,#2133,.T.);
#5261=EDGE_CURVE('',#4039,#4040,#2669,.T.);
#5262=EDGE_CURVE('',#4039,#4037,#2134,.T.);
#5263=EDGE_CURVE('',#4040,#4038,#2135,.T.);
#5264=EDGE_CURVE('',#4041,#4042,#2670,.T.);
#5265=EDGE_CURVE('',#4041,#4039,#2136,.T.);
#5266=EDGE_CURVE('',#4042,#4040,#2137,.T.);
#5267=EDGE_CURVE('',#4022,#4043,#2138,.T.);
#5268=EDGE_CURVE('',#4044,#4021,#2139,.T.);
#5269=EDGE_CURVE('',#4045,#4044,#1572,.T.);
#5270=EDGE_CURVE('',#4043,#4045,#2140,.T.);
#5271=EDGE_CURVE('',#4043,#4046,#2671,.T.);
#5272=EDGE_CURVE('',#4046,#4046,#1573,.T.);
#5273=EDGE_CURVE('',#4047,#4041,#2141,.T.);
#5274=EDGE_CURVE('',#3997,#4047,#2142,.T.);
#5275=EDGE_CURVE('',#4044,#4017,#2143,.T.);
#5276=EDGE_CURVE('',#4048,#4042,#2144,.T.);
#5277=EDGE_CURVE('',#4047,#4048,#1574,.T.);
#5278=EDGE_CURVE('',#4018,#4045,#2145,.T.);
#5279=EDGE_CURVE('',#4048,#3998,#2146,.T.);
#5280=EDGE_CURVE('',#4049,#4050,#2672,.T.);
#5281=EDGE_CURVE('',#4049,#4051,#2673,.T.);
#5282=EDGE_CURVE('',#4051,#4052,#2674,.T.);
#5283=EDGE_CURVE('',#4050,#4052,#2675,.T.);
#5284=EDGE_CURVE('',#4053,#4049,#2676,.T.);
#5285=EDGE_CURVE('',#4053,#4054,#2677,.T.);
#5286=EDGE_CURVE('',#4054,#4051,#2678,.T.);
#5287=EDGE_CURVE('',#4055,#4053,#2679,.T.);
#5288=EDGE_CURVE('',#4055,#4056,#2680,.T.);
#5289=EDGE_CURVE('',#4056,#4054,#2681,.T.);
#5290=EDGE_CURVE('',#4057,#4055,#2682,.T.);
#5291=EDGE_CURVE('',#4057,#4058,#2683,.T.);
#5292=EDGE_CURVE('',#4058,#4056,#2684,.T.);
#5293=EDGE_CURVE('',#4059,#4057,#2685,.T.);
#5294=EDGE_CURVE('',#4059,#4060,#2686,.T.);
#5295=EDGE_CURVE('',#4060,#4058,#2687,.T.);
#5296=EDGE_CURVE('',#4050,#4059,#2688,.T.);
#5297=EDGE_CURVE('',#4052,#4060,#2689,.T.);
#5298=EDGE_CURVE('',#4061,#4061,#1575,.T.);
#5299=EDGE_CURVE('',#4061,#4062,#2690,.T.);
#5300=EDGE_CURVE('',#4062,#4062,#1576,.T.);
#7551=ORIENTED_EDGE('',*,*,#5199,.F.);
#7552=ORIENTED_EDGE('',*,*,#5200,.T.);
#7553=ORIENTED_EDGE('',*,*,#5201,.T.);
#7554=ORIENTED_EDGE('',*,*,#5202,.T.);
#7555=ORIENTED_EDGE('',*,*,#5203,.F.);
#7556=ORIENTED_EDGE('',*,*,#5204,.T.);
#7557=ORIENTED_EDGE('',*,*,#5199,.T.);
#7558=ORIENTED_EDGE('',*,*,#5205,.T.);
#7559=ORIENTED_EDGE('',*,*,#5206,.F.);
#7560=ORIENTED_EDGE('',*,*,#5207,.T.);
#7561=ORIENTED_EDGE('',*,*,#5203,.T.);
#7562=ORIENTED_EDGE('',*,*,#5208,.T.);
#7563=ORIENTED_EDGE('',*,*,#5209,.F.);
#7564=ORIENTED_EDGE('',*,*,#5210,.T.);
#7565=ORIENTED_EDGE('',*,*,#5206,.T.);
#7566=ORIENTED_EDGE('',*,*,#5211,.T.);
#7567=ORIENTED_EDGE('',*,*,#5212,.F.);
#7568=ORIENTED_EDGE('',*,*,#5213,.T.);
#7569=ORIENTED_EDGE('',*,*,#5209,.T.);
#7570=ORIENTED_EDGE('',*,*,#5214,.T.);
#7571=ORIENTED_EDGE('',*,*,#5215,.F.);
#7572=ORIENTED_EDGE('',*,*,#5216,.T.);
#7573=ORIENTED_EDGE('',*,*,#5212,.T.);
#7574=ORIENTED_EDGE('',*,*,#5217,.T.);
#7575=ORIENTED_EDGE('',*,*,#5218,.F.);
#7576=ORIENTED_EDGE('',*,*,#5219,.T.);
#7577=ORIENTED_EDGE('',*,*,#5215,.T.);
#7578=ORIENTED_EDGE('',*,*,#5220,.T.);
#7579=ORIENTED_EDGE('',*,*,#5221,.F.);
#7580=ORIENTED_EDGE('',*,*,#5222,.T.);
#7581=ORIENTED_EDGE('',*,*,#5218,.T.);
#7582=ORIENTED_EDGE('',*,*,#5223,.T.);
#7583=ORIENTED_EDGE('',*,*,#5224,.F.);
#7584=ORIENTED_EDGE('',*,*,#5225,.T.);
#7585=ORIENTED_EDGE('',*,*,#5221,.T.);
#7586=ORIENTED_EDGE('',*,*,#5226,.T.);
#7587=ORIENTED_EDGE('',*,*,#5227,.F.);
#7588=ORIENTED_EDGE('',*,*,#5228,.T.);
#7589=ORIENTED_EDGE('',*,*,#5224,.T.);
#7590=ORIENTED_EDGE('',*,*,#5229,.T.);
#7591=ORIENTED_EDGE('',*,*,#5230,.F.);
#7592=ORIENTED_EDGE('',*,*,#5231,.T.);
#7593=ORIENTED_EDGE('',*,*,#5227,.T.);
#7594=ORIENTED_EDGE('',*,*,#5232,.T.);
#7595=ORIENTED_EDGE('',*,*,#5233,.F.);
#7596=ORIENTED_EDGE('',*,*,#5234,.T.);
#7597=ORIENTED_EDGE('',*,*,#5235,.T.);
#7598=ORIENTED_EDGE('',*,*,#5236,.F.);
#7599=ORIENTED_EDGE('',*,*,#5237,.F.);
#7600=ORIENTED_EDGE('',*,*,#5238,.T.);
#7601=ORIENTED_EDGE('',*,*,#5233,.T.);
#7602=ORIENTED_EDGE('',*,*,#5239,.F.);
#7603=ORIENTED_EDGE('',*,*,#5240,.F.);
#7604=ORIENTED_EDGE('',*,*,#5241,.T.);
#7605=ORIENTED_EDGE('',*,*,#5237,.T.);
#7606=ORIENTED_EDGE('',*,*,#5242,.F.);
#7607=ORIENTED_EDGE('',*,*,#5243,.F.);
#7608=ORIENTED_EDGE('',*,*,#5244,.T.);
#7609=ORIENTED_EDGE('',*,*,#5240,.T.);
#7610=ORIENTED_EDGE('',*,*,#5245,.F.);
#7611=ORIENTED_EDGE('',*,*,#5246,.F.);
#7612=ORIENTED_EDGE('',*,*,#5247,.T.);
#7613=ORIENTED_EDGE('',*,*,#5243,.T.);
#7614=ORIENTED_EDGE('',*,*,#5248,.F.);
#7615=ORIENTED_EDGE('',*,*,#5249,.F.);
#7616=ORIENTED_EDGE('',*,*,#5250,.T.);
#7617=ORIENTED_EDGE('',*,*,#5246,.T.);
#7618=ORIENTED_EDGE('',*,*,#5251,.F.);
#7619=ORIENTED_EDGE('',*,*,#5252,.F.);
#7620=ORIENTED_EDGE('',*,*,#5253,.T.);
#7621=ORIENTED_EDGE('',*,*,#5249,.T.);
#7622=ORIENTED_EDGE('',*,*,#5254,.F.);
#7623=ORIENTED_EDGE('',*,*,#5255,.F.);
#7624=ORIENTED_EDGE('',*,*,#5256,.T.);
#7625=ORIENTED_EDGE('',*,*,#5252,.T.);
#7626=ORIENTED_EDGE('',*,*,#5257,.F.);
#7627=ORIENTED_EDGE('',*,*,#5258,.F.);
#7628=ORIENTED_EDGE('',*,*,#5259,.T.);
#7629=ORIENTED_EDGE('',*,*,#5255,.T.);
#7630=ORIENTED_EDGE('',*,*,#5260,.F.);
#7631=ORIENTED_EDGE('',*,*,#5261,.F.);
#7632=ORIENTED_EDGE('',*,*,#5262,.T.);
#7633=ORIENTED_EDGE('',*,*,#5258,.T.);
#7634=ORIENTED_EDGE('',*,*,#5263,.F.);
#7635=ORIENTED_EDGE('',*,*,#5264,.F.);
#7636=ORIENTED_EDGE('',*,*,#5265,.T.);
#7637=ORIENTED_EDGE('',*,*,#5261,.T.);
#7638=ORIENTED_EDGE('',*,*,#5266,.F.);
#7639=ORIENTED_EDGE('',*,*,#5267,.F.);
#7640=ORIENTED_EDGE('',*,*,#5235,.F.);
#7641=ORIENTED_EDGE('',*,*,#5268,.F.);
#7642=ORIENTED_EDGE('',*,*,#5269,.F.);
#7643=ORIENTED_EDGE('',*,*,#5270,.F.);
#7644=ORIENTED_EDGE('',*,*,#5271,.T.);
#7645=ORIENTED_EDGE('',*,*,#5272,.F.);
#7646=ORIENTED_EDGE('',*,*,#5271,.F.);
#7647=ORIENTED_EDGE('',*,*,#5268,.T.);
#7648=ORIENTED_EDGE('',*,*,#5234,.F.);
#7649=ORIENTED_EDGE('',*,*,#5238,.F.);
#7650=ORIENTED_EDGE('',*,*,#5241,.F.);
#7651=ORIENTED_EDGE('',*,*,#5244,.F.);
#7652=ORIENTED_EDGE('',*,*,#5247,.F.);
#7653=ORIENTED_EDGE('',*,*,#5250,.F.);
#7654=ORIENTED_EDGE('',*,*,#5253,.F.);
#7655=ORIENTED_EDGE('',*,*,#5256,.F.);
#7656=ORIENTED_EDGE('',*,*,#5259,.F.);
#7657=ORIENTED_EDGE('',*,*,#5262,.F.);
#7658=ORIENTED_EDGE('',*,*,#5265,.F.);
#7659=ORIENTED_EDGE('',*,*,#5273,.F.);
#7660=ORIENTED_EDGE('',*,*,#5274,.F.);
#7661=ORIENTED_EDGE('',*,*,#5200,.F.);
#7662=ORIENTED_EDGE('',*,*,#5204,.F.);
#7663=ORIENTED_EDGE('',*,*,#5207,.F.);
#7664=ORIENTED_EDGE('',*,*,#5210,.F.);
#7665=ORIENTED_EDGE('',*,*,#5213,.F.);
#7666=ORIENTED_EDGE('',*,*,#5216,.F.);
#7667=ORIENTED_EDGE('',*,*,#5219,.F.);
#7668=ORIENTED_EDGE('',*,*,#5222,.F.);
#7669=ORIENTED_EDGE('',*,*,#5225,.F.);
#7670=ORIENTED_EDGE('',*,*,#5228,.F.);
#7671=ORIENTED_EDGE('',*,*,#5231,.F.);
#7672=ORIENTED_EDGE('',*,*,#5275,.F.);
#7673=ORIENTED_EDGE('',*,*,#5264,.T.);
#7674=ORIENTED_EDGE('',*,*,#5276,.F.);
#7675=ORIENTED_EDGE('',*,*,#5277,.F.);
#7676=ORIENTED_EDGE('',*,*,#5273,.T.);
#7677=ORIENTED_EDGE('',*,*,#5267,.T.);
#7678=ORIENTED_EDGE('',*,*,#5270,.T.);
#7679=ORIENTED_EDGE('',*,*,#5278,.F.);
#7680=ORIENTED_EDGE('',*,*,#5232,.F.);
#7681=ORIENTED_EDGE('',*,*,#5229,.F.);
#7682=ORIENTED_EDGE('',*,*,#5226,.F.);
#7683=ORIENTED_EDGE('',*,*,#5223,.F.);
#7684=ORIENTED_EDGE('',*,*,#5220,.F.);
#7685=ORIENTED_EDGE('',*,*,#5217,.F.);
#7686=ORIENTED_EDGE('',*,*,#5214,.F.);
#7687=ORIENTED_EDGE('',*,*,#5211,.F.);
#7688=ORIENTED_EDGE('',*,*,#5208,.F.);
#7689=ORIENTED_EDGE('',*,*,#5205,.F.);
#7690=ORIENTED_EDGE('',*,*,#5202,.F.);
#7691=ORIENTED_EDGE('',*,*,#5279,.F.);
#7692=ORIENTED_EDGE('',*,*,#5276,.T.);
#7693=ORIENTED_EDGE('',*,*,#5266,.T.);
#7694=ORIENTED_EDGE('',*,*,#5263,.T.);
#7695=ORIENTED_EDGE('',*,*,#5260,.T.);
#7696=ORIENTED_EDGE('',*,*,#5257,.T.);
#7697=ORIENTED_EDGE('',*,*,#5254,.T.);
#7698=ORIENTED_EDGE('',*,*,#5251,.T.);
#7699=ORIENTED_EDGE('',*,*,#5248,.T.);
#7700=ORIENTED_EDGE('',*,*,#5245,.T.);
#7701=ORIENTED_EDGE('',*,*,#5242,.T.);
#7702=ORIENTED_EDGE('',*,*,#5239,.T.);
#7703=ORIENTED_EDGE('',*,*,#5236,.T.);
#7704=ORIENTED_EDGE('',*,*,#5230,.T.);
#7705=ORIENTED_EDGE('',*,*,#5278,.T.);
#7706=ORIENTED_EDGE('',*,*,#5269,.T.);
#7707=ORIENTED_EDGE('',*,*,#5275,.T.);
#7708=ORIENTED_EDGE('',*,*,#5280,.F.);
#7709=ORIENTED_EDGE('',*,*,#5281,.T.);
#7710=ORIENTED_EDGE('',*,*,#5282,.T.);
#7711=ORIENTED_EDGE('',*,*,#5283,.F.);
#7712=ORIENTED_EDGE('',*,*,#5284,.F.);
#7713=ORIENTED_EDGE('',*,*,#5285,.T.);
#7714=ORIENTED_EDGE('',*,*,#5286,.T.);
#7715=ORIENTED_EDGE('',*,*,#5281,.F.);
#7716=ORIENTED_EDGE('',*,*,#5287,.F.);
#7717=ORIENTED_EDGE('',*,*,#5288,.T.);
#7718=ORIENTED_EDGE('',*,*,#5289,.T.);
#7719=ORIENTED_EDGE('',*,*,#5285,.F.);
#7720=ORIENTED_EDGE('',*,*,#5290,.F.);
#7721=ORIENTED_EDGE('',*,*,#5291,.T.);
#7722=ORIENTED_EDGE('',*,*,#5292,.T.);
#7723=ORIENTED_EDGE('',*,*,#5288,.F.);
#7724=ORIENTED_EDGE('',*,*,#5293,.F.);
#7725=ORIENTED_EDGE('',*,*,#5294,.T.);
#7726=ORIENTED_EDGE('',*,*,#5295,.T.);
#7727=ORIENTED_EDGE('',*,*,#5291,.F.);
#7728=ORIENTED_EDGE('',*,*,#5296,.F.);
#7729=ORIENTED_EDGE('',*,*,#5283,.T.);
#7730=ORIENTED_EDGE('',*,*,#5297,.T.);
#7731=ORIENTED_EDGE('',*,*,#5294,.F.);
#7732=ORIENTED_EDGE('',*,*,#5297,.F.);
#7733=ORIENTED_EDGE('',*,*,#5282,.F.);
#7734=ORIENTED_EDGE('',*,*,#5286,.F.);
#7735=ORIENTED_EDGE('',*,*,#5289,.F.);
#7736=ORIENTED_EDGE('',*,*,#5292,.F.);
#7737=ORIENTED_EDGE('',*,*,#5295,.F.);
#7738=ORIENTED_EDGE('',*,*,#5298,.T.);
#7739=ORIENTED_EDGE('',*,*,#5274,.T.);
#7740=ORIENTED_EDGE('',*,*,#5277,.T.);
#7741=ORIENTED_EDGE('',*,*,#5279,.T.);
#7742=ORIENTED_EDGE('',*,*,#5201,.F.);
#7743=ORIENTED_EDGE('',*,*,#5298,.F.);
#7744=ORIENTED_EDGE('',*,*,#5299,.T.);
#7745=ORIENTED_EDGE('',*,*,#5300,.T.);
#7746=ORIENTED_EDGE('',*,*,#5299,.F.);
#7747=ORIENTED_EDGE('',*,*,#5300,.F.);
#7748=ORIENTED_EDGE('',*,*,#5280,.T.);
#7749=ORIENTED_EDGE('',*,*,#5296,.T.);
#7750=ORIENTED_EDGE('',*,*,#5293,.T.);
#7751=ORIENTED_EDGE('',*,*,#5290,.T.);
#7752=ORIENTED_EDGE('',*,*,#5287,.T.);
#7753=ORIENTED_EDGE('',*,*,#5284,.T.);
#7754=ORIENTED_EDGE('',*,*,#5272,.T.);
#8161=CYLINDRICAL_SURFACE('',#9415,2.942);
#8162=CYLINDRICAL_SURFACE('',#9417,2.942);
#8163=CYLINDRICAL_SURFACE('',#9418,2.942);
#8164=CYLINDRICAL_SURFACE('',#9419,2.942);
#8165=CYLINDRICAL_SURFACE('',#9420,2.942);
#8166=CYLINDRICAL_SURFACE('',#9421,2.942);
#8167=CYLINDRICAL_SURFACE('',#9422,2.942);
#8168=CYLINDRICAL_SURFACE('',#9423,2.942);
#8169=CYLINDRICAL_SURFACE('',#9424,2.942);
#8170=CYLINDRICAL_SURFACE('',#9425,2.942);
#8171=CYLINDRICAL_SURFACE('',#9426,2.942);
#8172=CYLINDRICAL_SURFACE('',#9427,2.37175);
#8173=CYLINDRICAL_SURFACE('',#9429,2.37175);
#8174=CYLINDRICAL_SURFACE('',#9430,2.37175);
#8175=CYLINDRICAL_SURFACE('',#9431,2.37175);
#8176=CYLINDRICAL_SURFACE('',#9432,2.37175);
#8177=CYLINDRICAL_SURFACE('',#9433,2.37175);
#8178=CYLINDRICAL_SURFACE('',#9434,2.37175);
#8179=CYLINDRICAL_SURFACE('',#9435,2.37175);
#8180=CYLINDRICAL_SURFACE('',#9436,2.37175);
#8181=CYLINDRICAL_SURFACE('',#9437,2.37175);
#8182=CYLINDRICAL_SURFACE('',#9438,2.37175);
#8183=CYLINDRICAL_SURFACE('',#9442,2.37175);
#8184=CYLINDRICAL_SURFACE('',#9444,2.942);
#8185=CYLINDRICAL_SURFACE('',#9454,5.);
#8611=ADVANCED_FACE('',(#863),#8161,.T.);
#8612=ADVANCED_FACE('',(#864),#8162,.T.);
#8613=ADVANCED_FACE('',(#865),#8163,.T.);
#8614=ADVANCED_FACE('',(#866),#8164,.T.);
#8615=ADVANCED_FACE('',(#867),#8165,.T.);
#8616=ADVANCED_FACE('',(#868),#8166,.T.);
#8617=ADVANCED_FACE('',(#869),#8167,.T.);
#8618=ADVANCED_FACE('',(#870),#8168,.T.);
#8619=ADVANCED_FACE('',(#871),#8169,.T.);
#8620=ADVANCED_FACE('',(#872),#8170,.T.);
#8621=ADVANCED_FACE('',(#873),#8171,.T.);
#8622=ADVANCED_FACE('',(#874),#8172,.T.);
#8623=ADVANCED_FACE('',(#875),#8173,.T.);
#8624=ADVANCED_FACE('',(#876),#8174,.T.);
#8625=ADVANCED_FACE('',(#877),#8175,.T.);
#8626=ADVANCED_FACE('',(#878),#8176,.T.);
#8627=ADVANCED_FACE('',(#879),#8177,.T.);
#8628=ADVANCED_FACE('',(#880),#8178,.T.);
#8629=ADVANCED_FACE('',(#881),#8179,.T.);
#8630=ADVANCED_FACE('',(#882),#8180,.T.);
#8631=ADVANCED_FACE('',(#883),#8181,.T.);
#8632=ADVANCED_FACE('',(#884),#8182,.T.);
#8633=ADVANCED_FACE('',(#885),#161,.T.);
#8634=ADVANCED_FACE('',(#886),#307,.F.);
#8635=ADVANCED_FACE('',(#887),#8183,.T.);
#8636=ADVANCED_FACE('',(#888),#308,.F.);
#8637=ADVANCED_FACE('',(#889),#8184,.T.);
#8638=ADVANCED_FACE('',(#890),#432,.F.);
#8639=ADVANCED_FACE('',(#891),#433,.F.);
#8640=ADVANCED_FACE('',(#892),#434,.F.);
#8641=ADVANCED_FACE('',(#893),#435,.F.);
#8642=ADVANCED_FACE('',(#894),#436,.F.);
#8643=ADVANCED_FACE('',(#895),#437,.F.);
#8644=ADVANCED_FACE('',(#896),#438,.F.);
#8645=ADVANCED_FACE('',(#897,#287),#439,.T.);
#8646=ADVANCED_FACE('',(#898),#8185,.T.);
#8647=ADVANCED_FACE('',(#899,#288),#440,.F.);
#8648=ADVANCED_FACE('',(#900),#441,.T.);
#8690=CLOSED_SHELL('',(#8611,#8612,#8613,#8614,#8615,#8616,#8617,#8618,
#8619,#8620,#8621,#8622,#8623,#8624,#8625,#8626,#8627,#8628,#8629,#8630,
#8631,#8632,#8633,#8634,#8635,#8636,#8637,#8638,#8639,#8640,#8641,#8642,
#8643,#8644,#8645,#8646,#8647,#8648));
#9414=AXIS2_PLACEMENT_3D('',#29418,#11047,#11048);
#9415=AXIS2_PLACEMENT_3D('',#29419,#11049,#11050);
#9416=AXIS2_PLACEMENT_3D('',#29435,#11052,#11053);
#9417=AXIS2_PLACEMENT_3D('',#29443,#11054,#11055);
#9418=AXIS2_PLACEMENT_3D('',#29491,#11057,#11058);
#9419=AXIS2_PLACEMENT_3D('',#29539,#11060,#11061);
#9420=AXIS2_PLACEMENT_3D('',#29593,#11063,#11064);
#9421=AXIS2_PLACEMENT_3D('',#29641,#11066,#11067);
#9422=AXIS2_PLACEMENT_3D('',#29689,#11069,#11070);
#9423=AXIS2_PLACEMENT_3D('',#29743,#11072,#11073);
#9424=AXIS2_PLACEMENT_3D('',#29791,#11075,#11076);
#9425=AXIS2_PLACEMENT_3D('',#29842,#11078,#11079);
#9426=AXIS2_PLACEMENT_3D('',#29893,#11081,#11082);
#9427=AXIS2_PLACEMENT_3D('',#29941,#11084,#11085);
#9428=AXIS2_PLACEMENT_3D('',#29957,#11087,#11088);
#9429=AXIS2_PLACEMENT_3D('',#29966,#11089,#11090);
#9430=AXIS2_PLACEMENT_3D('',#29991,#11092,#11093);
#9431=AXIS2_PLACEMENT_3D('',#30015,#11095,#11096);
#9432=AXIS2_PLACEMENT_3D('',#30041,#11098,#11099);
#9433=AXIS2_PLACEMENT_3D('',#30065,#11101,#11102);
#9434=AXIS2_PLACEMENT_3D('',#30090,#11104,#11105);
#9435=AXIS2_PLACEMENT_3D('',#30115,#11107,#11108);
#9436=AXIS2_PLACEMENT_3D('',#30139,#11110,#11111);
#9437=AXIS2_PLACEMENT_3D('',#30164,#11113,#11114);
#9438=AXIS2_PLACEMENT_3D('',#30189,#11116,#11117);
#9439=AXIS2_PLACEMENT_3D('',#30213,#11119,#11120);
#9440=AXIS2_PLACEMENT_3D('',#30495,#11121,#11122);
#9441=AXIS2_PLACEMENT_3D('',#30529,#11124,#11125);
#9442=AXIS2_PLACEMENT_3D('',#30954,#11126,#11127);
#9443=AXIS2_PLACEMENT_3D('',#30965,#11128,#11129);
#9444=AXIS2_PLACEMENT_3D('',#31392,#11130,#11131);
#9445=AXIS2_PLACEMENT_3D('',#31393,#11132,#11133);
#9446=AXIS2_PLACEMENT_3D('',#31402,#11138,#11139);
#9447=AXIS2_PLACEMENT_3D('',#31408,#11143,#11144);
#9448=AXIS2_PLACEMENT_3D('',#31414,#11148,#11149);
#9449=AXIS2_PLACEMENT_3D('',#31420,#11153,#11154);
#9450=AXIS2_PLACEMENT_3D('',#31426,#11158,#11159);
#9451=AXIS2_PLACEMENT_3D('',#31429,#11162,#11163);
#9452=AXIS2_PLACEMENT_3D('',#31430,#11164,#11165);
#9453=AXIS2_PLACEMENT_3D('',#31432,#11166,#11167);
#9454=AXIS2_PLACEMENT_3D('',#31433,#11168,#11169);
#9455=AXIS2_PLACEMENT_3D('',#31436,#11171,#11172);
#9456=AXIS2_PLACEMENT_3D('',#31437,#11173,#11174);
#9457=AXIS2_PLACEMENT_3D('',#31438,#11175,#11176);
#11047=DIRECTION('axis',(0.,0.,1.));
#11048=DIRECTION('refdir',(1.,0.,0.));
#11049=DIRECTION('center_axis',(0.,0.,1.));
#11050=DIRECTION('ref_axis',(1.,0.,0.));
#11051=DIRECTION('',(0.,0.,-1.));
#11052=DIRECTION('center_axis',(0.,0.,-1.));
#11053=DIRECTION('ref_axis',(1.,0.,0.));
#11054=DIRECTION('center_axis',(0.,0.,1.));
#11055=DIRECTION('ref_axis',(1.,0.,0.));
#11056=DIRECTION('',(0.,0.,-1.));
#11057=DIRECTION('center_axis',(0.,0.,1.));
#11058=DIRECTION('ref_axis',(1.,0.,0.));
#11059=DIRECTION('',(0.,0.,-1.));
#11060=DIRECTION('center_axis',(0.,0.,1.));
#11061=DIRECTION('ref_axis',(1.,0.,0.));
#11062=DIRECTION('',(0.,0.,-1.));
#11063=DIRECTION('center_axis',(0.,0.,1.));
#11064=DIRECTION('ref_axis',(1.,0.,0.));
#11065=DIRECTION('',(0.,0.,-1.));
#11066=DIRECTION('center_axis',(0.,0.,1.));
#11067=DIRECTION('ref_axis',(1.,0.,0.));
#11068=DIRECTION('',(0.,0.,-1.));
#11069=DIRECTION('center_axis',(0.,0.,1.));
#11070=DIRECTION('ref_axis',(1.,0.,0.));
#11071=DIRECTION('',(0.,0.,-1.));
#11072=DIRECTION('center_axis',(0.,0.,1.));
#11073=DIRECTION('ref_axis',(1.,0.,0.));
#11074=DIRECTION('',(0.,0.,-1.));
#11075=DIRECTION('center_axis',(0.,0.,1.));
#11076=DIRECTION('ref_axis',(1.,0.,0.));
#11077=DIRECTION('',(0.,0.,-1.));
#11078=DIRECTION('center_axis',(0.,0.,1.));
#11079=DIRECTION('ref_axis',(1.,0.,0.));
#11080=DIRECTION('',(0.,0.,-1.));
#11081=DIRECTION('center_axis',(0.,0.,1.));
#11082=DIRECTION('ref_axis',(1.,0.,0.));
#11083=DIRECTION('',(0.,0.,-1.));
#11084=DIRECTION('center_axis',(0.,0.,1.));
#11085=DIRECTION('ref_axis',(0.997344302588954,-0.0728309144069492,0.));
#11086=DIRECTION('',(0.,0.,1.));
#11087=DIRECTION('center_axis',(0.,0.,-1.));
#11088=DIRECTION('ref_axis',(1.,7.52212518638754E-14,0.));
#11089=DIRECTION('center_axis',(0.,0.,1.));
#11090=DIRECTION('ref_axis',(1.,7.52212518638754E-14,0.));
#11091=DIRECTION('',(0.,0.,1.));
#11092=DIRECTION('center_axis',(0.,0.,1.));
#11093=DIRECTION('ref_axis',(1.,7.52212518638754E-14,0.));
#11094=DIRECTION('',(0.,0.,1.));
#11095=DIRECTION('center_axis',(0.,0.,1.));
#11096=DIRECTION('ref_axis',(1.,7.52212518638754E-14,0.));
#11097=DIRECTION('',(0.,0.,1.));
#11098=DIRECTION('center_axis',(0.,0.,1.));
#11099=DIRECTION('ref_axis',(1.,7.52212518638754E-14,0.));
#11100=DIRECTION('',(0.,0.,1.));
#11101=DIRECTION('center_axis',(0.,0.,1.));
#11102=DIRECTION('ref_axis',(1.,7.52212518638754E-14,0.));
#11103=DIRECTION('',(0.,0.,1.));
#11104=DIRECTION('center_axis',(0.,0.,1.));
#11105=DIRECTION('ref_axis',(1.,7.52212518638754E-14,0.));
#11106=DIRECTION('',(0.,0.,1.));
#11107=DIRECTION('center_axis',(0.,0.,1.));
#11108=DIRECTION('ref_axis',(1.,7.52212518638754E-14,0.));
#11109=DIRECTION('',(0.,0.,1.));
#11110=DIRECTION('center_axis',(0.,0.,1.));
#11111=DIRECTION('ref_axis',(1.,7.52212518638754E-14,0.));
#11112=DIRECTION('',(0.,0.,1.));
#11113=DIRECTION('center_axis',(0.,0.,1.));
#11114=DIRECTION('ref_axis',(1.,7.52212518638754E-14,0.));
#11115=DIRECTION('',(0.,0.,1.));
#11116=DIRECTION('center_axis',(0.,0.,1.));
#11117=DIRECTION('ref_axis',(1.,7.52212518638754E-14,0.));
#11118=DIRECTION('',(0.,0.,1.));
#11119=DIRECTION('center_axis',(0.,0.,-1.));
#11120=DIRECTION('ref_axis',(1.,0.,0.));
#11121=DIRECTION('center_axis',(0.,0.,-1.));
#11122=DIRECTION('ref_axis',(1.,0.,0.));
#11123=DIRECTION('',(0.707106781186548,8.65956056235494E-17,0.707106781186547));
#11124=DIRECTION('center_axis',(0.,0.,1.));
#11125=DIRECTION('ref_axis',(1.,0.,0.));
#11126=DIRECTION('center_axis',(0.,0.,1.));
#11127=DIRECTION('ref_axis',(1.,7.52212518638754E-14,0.));
#11128=DIRECTION('center_axis',(0.,0.,-1.));
#11129=DIRECTION('ref_axis',(1.,7.52212518638754E-14,0.));
#11130=DIRECTION('center_axis',(0.,0.,1.));
#11131=DIRECTION('ref_axis',(1.,0.,0.));
#11132=DIRECTION('center_axis',(-1.92296268638356E-16,-1.,0.));
#11133=DIRECTION('ref_axis',(1.,-1.92296268638356E-16,0.));
#11134=DIRECTION('',(1.,-1.92296268638356E-16,0.));
#11135=DIRECTION('',(0.,0.,1.));
#11136=DIRECTION('',(1.,-1.92296268638356E-16,0.));
#11137=DIRECTION('',(0.,0.,1.));
#11138=DIRECTION('center_axis',(-0.866025403784439,-0.5,0.));
#11139=DIRECTION('ref_axis',(0.5,-0.866025403784439,0.));
#11140=DIRECTION('',(0.5,-0.866025403784439,0.));
#11141=DIRECTION('',(0.,0.,1.));
#11142=DIRECTION('',(0.5,-0.866025403784439,0.));
#11143=DIRECTION('center_axis',(-0.866025403784439,0.5,0.));
#11144=DIRECTION('ref_axis',(-0.5,-0.866025403784438,0.));
#11145=DIRECTION('',(-0.5,-0.866025403784438,0.));
#11146=DIRECTION('',(0.,0.,1.));
#11147=DIRECTION('',(-0.5,-0.866025403784439,0.));
#11148=DIRECTION('center_axis',(1.92296268638356E-16,1.,0.));
#11149=DIRECTION('ref_axis',(-1.,1.92296268638356E-16,0.));
#11150=DIRECTION('',(-1.,1.92296268638356E-16,0.));
#11151=DIRECTION('',(0.,0.,1.));
#11152=DIRECTION('',(-1.,1.92296268638356E-16,0.));
#11153=DIRECTION('center_axis',(0.866025403784439,0.5,0.));
#11154=DIRECTION('ref_axis',(-0.5,0.866025403784439,0.));
#11155=DIRECTION('',(-0.5,0.866025403784439,0.));
#11156=DIRECTION('',(0.,0.,1.));
#11157=DIRECTION('',(-0.5,0.866025403784439,0.));
#11158=DIRECTION('center_axis',(0.866025403784439,-0.5,0.));
#11159=DIRECTION('ref_axis',(0.5,0.866025403784439,0.));
#11160=DIRECTION('',(0.5,0.866025403784439,0.));
#11161=DIRECTION('',(0.5,0.866025403784439,0.));
#11162=DIRECTION('center_axis',(0.,0.,1.));
#11163=DIRECTION('ref_axis',(1.,0.,0.));
#11164=DIRECTION('center_axis',(0.,0.,1.));
#11165=DIRECTION('ref_axis',(1.,0.,0.));
#11166=DIRECTION('center_axis',(0.,0.,1.));
#11167=DIRECTION('ref_axis',(1.,0.,0.));
#11168=DIRECTION('center_axis',(0.,0.,1.));
#11169=DIRECTION('ref_axis',(1.,0.,0.));
#11170=DIRECTION('',(0.,0.,-1.));
#11171=DIRECTION('center_axis',(0.,0.,1.));
#11172=DIRECTION('ref_axis',(1.,0.,0.));
#11173=DIRECTION('center_axis',(0.,0.,1.));
#11174=DIRECTION('ref_axis',(1.,0.,0.));
#11175=DIRECTION('center_axis',(0.,0.,1.));
#11176=DIRECTION('ref_axis',(1.,0.,0.));
#29418=CARTESIAN_POINT('',(0.,0.,0.));
#29419=CARTESIAN_POINT('Origin',(0.,0.,0.));
#29420=CARTESIAN_POINT('',(-2.94437861999191,0.00228824954296311,0.322176117089596));
#29421=CARTESIAN_POINT('',(-2.94436911647834,0.00312614869137163,0.177823882910396));
#29422=CARTESIAN_POINT('',(-2.942,-3.60291088309151E-16,0.));
#29423=CARTESIAN_POINT('',(1.28892185405323,2.64462557919717,0.));
#29424=CARTESIAN_POINT('Ctrl Pts',(-2.94437861999191,0.00228824954296311,
0.322176117089596));
#29425=CARTESIAN_POINT('Ctrl Pts',(-2.94551635113874,0.142778583613822,
0.314557432409286));
#29426=CARTESIAN_POINT('Ctrl Pts',(-2.93631267309395,0.283111895578672,
0.306938747728977));
#29427=CARTESIAN_POINT('Ctrl Pts',(-2.91624915612822,0.42186500989966,0.299320063048668));
#29428=CARTESIAN_POINT('Ctrl Pts',(-2.77830971889191,1.37581174500659,0.246940558544163));
#29429=CARTESIAN_POINT('Ctrl Pts',(-2.1270526803082,2.25506646395135,0.194561054039658));
#29430=CARTESIAN_POINT('Ctrl Pts',(-1.25475282359973,2.66583045735473,0.142181549535154));
#29431=CARTESIAN_POINT('Ctrl Pts',(-0.46548135530728,3.03749657388775,0.0947876996901026));
#29432=CARTESIAN_POINT('Ctrl Pts',(0.504756374147381,3.02561249996607,0.0473938498450515));
#29433=CARTESIAN_POINT('Ctrl Pts',(1.29197400994443,2.64783394680711,3.05745012640912E-16));
#29434=CARTESIAN_POINT('',(-1.28892185405326,2.64462557919716,0.));
#29435=CARTESIAN_POINT('Origin',(0.,0.,0.));
#29436=CARTESIAN_POINT('Ctrl Pts',(-1.28892185405326,2.64462557919716,1.87350135405495E-15));
#29437=CARTESIAN_POINT('Ctrl Pts',(-2.16038499609478,2.21989706654312,0.0524451052237091));
#29438=CARTESIAN_POINT('Ctrl Pts',(-2.79846764402885,1.33473338532309,0.104890210447416));
#29439=CARTESIAN_POINT('Ctrl Pts',(-2.92193100282573,0.379041548713593,
0.157335315671123));
#29440=CARTESIAN_POINT('Ctrl Pts',(-2.93800868581449,0.25458915624929,0.164164838084214));
#29441=CARTESIAN_POINT('Ctrl Pts',(-2.94535953294187,0.128940758021734,
0.170994360497305));
#29442=CARTESIAN_POINT('Ctrl Pts',(-2.94436911647834,0.00312614869137163,
0.177823882910396));
#29443=CARTESIAN_POINT('Origin',(0.,0.,0.));
#29444=CARTESIAN_POINT('',(-2.93740032720055,-0.000139020310086779,1.32217611708959));
#29445=CARTESIAN_POINT('',(-2.93737720095951,0.000230872487724698,1.1778238829104));
#29446=CARTESIAN_POINT('',(-2.942,-3.60291088309151E-16,0.));
#29447=CARTESIAN_POINT('Ctrl Pts',(-2.93740032720055,-0.000139020310086779,
1.32217611708959));
#29448=CARTESIAN_POINT('Ctrl Pts',(-2.93718361365059,0.494770241727901,
1.29550112610298));
#29449=CARTESIAN_POINT('Ctrl Pts',(-2.81848923912434,0.989776479202536,
1.26882613511636));
#29450=CARTESIAN_POINT('Ctrl Pts',(-2.58191143461274,1.4199490257311,1.24215114412975));
#29451=CARTESIAN_POINT('Ctrl Pts',(-2.11736289237333,2.26464377557798,1.18977163962524));
#29452=CARTESIAN_POINT('Ctrl Pts',(-1.19827972440715,2.85935294685526,1.13739213512074));
#29453=CARTESIAN_POINT('Ctrl Pts',(-0.2374000875181,2.93702585155106,1.08501263061624));
#29454=CARTESIAN_POINT('Ctrl Pts',(0.723479549370952,3.01469875624685,1.03263312611173));
#29455=CARTESIAN_POINT('Ctrl Pts',(1.72615565518287,2.57533539436116,0.980253621607226));
#29456=CARTESIAN_POINT('Ctrl Pts',(2.32033868002489,1.8162041612206,0.927874117102722));
#29457=CARTESIAN_POINT('Ctrl Pts',(2.9145217048669,1.05707292808004,0.875494612598217));
#29458=CARTESIAN_POINT('Ctrl Pts',(3.100211648739,-0.0218261763153739,0.823115108093712));
#29459=CARTESIAN_POINT('Ctrl Pts',(2.79403320730894,-0.935902477435646,
0.770735603589208));
#29460=CARTESIAN_POINT('Ctrl Pts',(2.48785476587888,-1.84997877855592,0.718356099084703));
#29461=CARTESIAN_POINT('Ctrl Pts',(1.68980793914667,-2.59923227640105,0.665976594580199));
#29462=CARTESIAN_POINT('Ctrl Pts',(0.75825229618776,-2.84733793424016,0.613597090075694));
#29463=CARTESIAN_POINT('Ctrl Pts',(-0.173303346771145,-3.09544359207927,
0.56121758557119));
#29464=CARTESIAN_POINT('Ctrl Pts',(-1.23836780595674,-2.84240140991237,
0.508838081066685));
#29465=CARTESIAN_POINT('Ctrl Pts',(-1.95858911760509,-2.20156094319437,
0.456458576562181));
#29466=CARTESIAN_POINT('Ctrl Pts',(-2.57405306040479,-1.65393177147606,
0.411697756737986));
#29467=CARTESIAN_POINT('Ctrl Pts',(-2.93769429310237,-0.823111776086056,
0.366936936913791));
#29468=CARTESIAN_POINT('Ctrl Pts',(-2.94437861999191,0.00228824954296311,
0.322176117089596));
#29469=CARTESIAN_POINT('Ctrl Pts',(-2.94436911647834,0.00312614869137163,
0.177823882910396));
#29470=CARTESIAN_POINT('Ctrl Pts',(-2.93775395051561,-0.837211781775621,
0.223439465721013));
#29471=CARTESIAN_POINT('Ctrl Pts',(-2.55902339432207,-1.68496462111194,
0.26905504853163));
#29472=CARTESIAN_POINT('Ctrl Pts',(-1.92306539600717,-2.23328718212897,
0.314670631342247));
#29473=CARTESIAN_POINT('Ctrl Pts',(-1.19189236073203,-2.86370408436305,
0.367115736565955));
#29474=CARTESIAN_POINT('Ctrl Pts',(-0.120702220522052,-3.09831789683223,
0.419560841789662));
#29475=CARTESIAN_POINT('Ctrl Pts',(0.807638005699694,-2.8335361097114,0.47200594701337));
#29476=CARTESIAN_POINT('Ctrl Pts',(1.73597823192144,-2.56875432259058,0.524451052237078));
#29477=CARTESIAN_POINT('Ctrl Pts',(2.52146854415495,-1.80457693587975,0.576896157460787));
#29478=CARTESIAN_POINT('Ctrl Pts',(2.81091642121069,-0.883954119006901,
0.629341262684494));
#29479=CARTESIAN_POINT('Ctrl Pts',(3.10036429826643,0.0366686978659464,
0.681786367908202));
#29480=CARTESIAN_POINT('Ctrl Pts',(2.89376974014439,1.11373694490081,0.734231473131909));
#29481=CARTESIAN_POINT('Ctrl Pts',(2.28393241469019,1.86192138048068,0.786676578355617));
#29482=CARTESIAN_POINT('Ctrl Pts',(1.674095089236,2.61010581606054,0.839121683579324));
#29483=CARTESIAN_POINT('Ctrl Pts',(0.661014996449636,3.02940644018541,0.891566788803033));
#29484=CARTESIAN_POINT('Ctrl Pts',(-0.299207810136722,2.93136603044105,
0.944011894026741));
#29485=CARTESIAN_POINT('Ctrl Pts',(-1.25943061672308,2.83332562069669,0.996456999250449));
#29486=CARTESIAN_POINT('Ctrl Pts',(-2.16679613710945,2.21794417708309,1.04890210447416));
#29487=CARTESIAN_POINT('Ctrl Pts',(-2.61293993368518,1.36206873790977,1.10134720969786));
#29488=CARTESIAN_POINT('Ctrl Pts',(-2.82979902340055,0.946049575313678,
1.12683943410204));
#29489=CARTESIAN_POINT('Ctrl Pts',(-2.93768601866802,0.47320929383844,1.15233165850622));
#29490=CARTESIAN_POINT('Ctrl Pts',(-2.93737720095951,0.000230872487724698,
1.1778238829104));
#29491=CARTESIAN_POINT('Origin',(0.,0.,0.));
#29492=CARTESIAN_POINT('',(-2.94487182720719,-0.00190539986535287,2.32217611708959));
#29493=CARTESIAN_POINT('',(-2.94409804542743,-0.00221960462873976,2.1778238829104));
#29494=CARTESIAN_POINT('',(-2.942,-3.60291088309151E-16,0.));
#29495=CARTESIAN_POINT('Ctrl Pts',(-2.94487182720719,-0.00190539986535287,
2.32217611708959));
#29496=CARTESIAN_POINT('Ctrl Pts',(-2.93849254859689,0.841069663508672,
2.27644481979667));
#29497=CARTESIAN_POINT('Ctrl Pts',(-2.55692453936773,1.68909389771769,2.23071352250375));
#29498=CARTESIAN_POINT('Ctrl Pts',(-1.91797659724234,2.23693579382214,2.18498222521083));
#29499=CARTESIAN_POINT('Ctrl Pts',(-1.18614132044426,2.86442044357863,2.13260272070633));
#29500=CARTESIAN_POINT('Ctrl Pts',(-0.116653199765081,3.09810042098425,
2.08022321620182));
#29501=CARTESIAN_POINT('Ctrl Pts',(0.810201861614963,2.83303510458914,2.02784371169732));
#29502=CARTESIAN_POINT('Ctrl Pts',(1.73705692299501,2.56796978819403,1.97546420719281));
#29503=CARTESIAN_POINT('Ctrl Pts',(2.52127892507592,1.80415917799819,1.92308470268831));
#29504=CARTESIAN_POINT('Ctrl Pts',(2.81068910755427,0.88461468761641,1.8707051981838));
#29505=CARTESIAN_POINT('Ctrl Pts',(3.10009929003262,-0.0349298027653776,
1.8183256936793));
#29506=CARTESIAN_POINT('Ctrl Pts',(2.89469765290841,-1.11020817333311,1.76594618917479));
#29507=CARTESIAN_POINT('Ctrl Pts',(2.28672630753671,-1.85833254788295,1.71356668467029));
#29508=CARTESIAN_POINT('Ctrl Pts',(1.67875496216501,-2.60645692243279,1.66118718016578));
#29509=CARTESIAN_POINT('Ctrl Pts',(0.668213908545816,-3.02742730096473,
1.60880767566128));
#29510=CARTESIAN_POINT('Ctrl Pts',(-0.291083395731117,-2.93219727380604,
1.55642817115678));
#29511=CARTESIAN_POINT('Ctrl Pts',(-1.25038070000804,-2.83696724664735,
1.50404866665227));
#29512=CARTESIAN_POINT('Ctrl Pts',(-2.15843425494271,-2.22553681379804,
1.45166916214777));
#29513=CARTESIAN_POINT('Ctrl Pts',(-2.60745407415374,-1.37248143316515,
1.39928965764326));
#29514=CARTESIAN_POINT('Ctrl Pts',(-2.82780430697652,-0.953856366540085,
1.37358514412537));
#29515=CARTESIAN_POINT('Ctrl Pts',(-2.93760915637607,-0.477042717206063,
1.34788063060748));
#29516=CARTESIAN_POINT('Ctrl Pts',(-2.93740032720055,-0.000139020310086779,
1.32217611708959));
#29517=CARTESIAN_POINT('Ctrl Pts',(-2.93737720095951,0.000230872487724698,
1.1778238829104));
#29518=CARTESIAN_POINT('Ctrl Pts',(-2.9370506885783,-0.499848321024544,
1.20477676372993));
#29519=CARTESIAN_POINT('Ctrl Pts',(-2.81577431600542,-1.00008193824477,
1.23172964454946));
#29520=CARTESIAN_POINT('Ctrl Pts',(-2.57446559490686,-1.43347457044749,
1.25868252536899));
#29521=CARTESIAN_POINT('Ctrl Pts',(-2.10492538678771,-2.27677300489839,
1.31112763059269));
#29522=CARTESIAN_POINT('Ctrl Pts',(-1.1809228977843,-2.86700043906715,1.3635727358164));
#29523=CARTESIAN_POINT('Ctrl Pts',(-0.218377608724914,-2.93852741234213,
1.41601784104011));
#29524=CARTESIAN_POINT('Ctrl Pts',(0.744167680334467,-3.01005438561711,
1.46846294626382));
#29525=CARTESIAN_POINT('Ctrl Pts',(1.74525576944982,-2.56288089799832,1.52090805148753));
#29526=CARTESIAN_POINT('Ctrl Pts',(2.33429173832943,-1.79826479808332,1.57335315671123));
#29527=CARTESIAN_POINT('Ctrl Pts',(2.92332770720905,-1.03364869816832,1.62579826193494));
#29528=CARTESIAN_POINT('Ctrl Pts',(3.10031155585293,0.0484100140428809,
1.67824336715865));
#29529=CARTESIAN_POINT('Ctrl Pts',(2.78557670999694,0.960852278151669,1.73068847238236));
#29530=CARTESIAN_POINT('Ctrl Pts',(2.47084186414094,1.87329454226046,1.78313357760607));
#29531=CARTESIAN_POINT('Ctrl Pts',(1.66438832378506,2.61612035826684,1.83557868282977));
#29532=CARTESIAN_POINT('Ctrl Pts',(0.729213057861966,2.85498007465664,1.88802378805348));
#29533=CARTESIAN_POINT('Ctrl Pts',(-0.205962208061124,3.09383979104644,
1.94046889327719));
#29534=CARTESIAN_POINT('Ctrl Pts',(-1.26985919955142,2.82873340781965,1.9929139985009));
#29535=CARTESIAN_POINT('Ctrl Pts',(-1.98360551176881,2.17898571169394,2.0453591037246));
#29536=CARTESIAN_POINT('Ctrl Pts',(-2.58452748049057,1.63194587688865,2.08951403011987));
#29537=CARTESIAN_POINT('Ctrl Pts',(-2.93724853244873,0.81225677381718,2.13366895651513));
#29538=CARTESIAN_POINT('Ctrl Pts',(-2.94409804542743,-0.00221960462873976,
2.1778238829104));
#29539=CARTESIAN_POINT('Origin',(0.,0.,0.));
#29540=CARTESIAN_POINT('',(-2.94188729812012,0.00254759896953657,3.32217611708959));
#29541=CARTESIAN_POINT('',(-2.94300132914192,0.00247067809074119,3.17782388291039));
#29542=CARTESIAN_POINT('',(-2.942,-3.60291088309151E-16,0.));
#29543=CARTESIAN_POINT('Ctrl Pts',(-2.94188729812012,0.00254759896953657,
3.32217611708959));
#29544=CARTESIAN_POINT('Ctrl Pts',(-2.94391723822425,0.231870355671395,
3.30976801799487));
#29545=CARTESIAN_POINT('Ctrl Pts',(-2.91930872547992,0.460762551320829,
3.29735991890015));
#29546=CARTESIAN_POINT('Ctrl Pts',(-2.86638309031571,0.682908266801983,
3.28495181980542));
#29547=CARTESIAN_POINT('Ctrl Pts',(-2.64296300603654,1.62067338423639,3.23257231530092));
#29548=CARTESIAN_POINT('Ctrl Pts',(-1.91492649555138,2.438214961245,3.18019281079642));
#29549=CARTESIAN_POINT('Ctrl Pts',(-1.00922037183541,2.76839122410029,3.12781330629191));
#29550=CARTESIAN_POINT('Ctrl Pts',(-0.103514248119433,3.09856748695557,
3.07543380178741));
#29551=CARTESIAN_POINT('Ctrl Pts',(0.979861488827348,2.94137843565753,3.0230542972829));
#29552=CARTESIAN_POINT('Ctrl Pts',(1.75438420282982,2.3674145763557,2.9706747927784));
#29553=CARTESIAN_POINT('Ctrl Pts',(2.5289069168323,1.79345071705387,2.91829528827389));
#29554=CARTESIAN_POINT('Ctrl Pts',(2.99457660789046,0.802712049748258,2.86591578376939));
#29555=CARTESIAN_POINT('Ctrl Pts',(2.94227021542597,-0.159880282562335,
2.81353627926488));
#29556=CARTESIAN_POINT('Ctrl Pts',(2.88996382296149,-1.12247261487293,2.76115677476038));
#29557=CARTESIAN_POINT('Ctrl Pts',(2.31968134697434,-2.0569186121885,2.70877727025587));
#29558=CARTESIAN_POINT('Ctrl Pts',(1.48752538566269,-2.54357700727495,2.65639776575137));
#29559=CARTESIAN_POINT('Ctrl Pts',(0.655369424351043,-3.0302354023614,2.60401826124687));
#29560=CARTESIAN_POINT('Ctrl Pts',(-0.438660022285117,-3.06910619521874,
2.55163875674236));
#29561=CARTESIAN_POINT('Ctrl Pts',(-1.30325595742871,-2.64273334365957,
2.49925925223786));
#29562=CARTESIAN_POINT('Ctrl Pts',(-2.1678518925723,-2.21636049210041,2.44687974773335));
#29563=CARTESIAN_POINT('Ctrl Pts',(-2.80301431622333,-1.32474399612474,
2.39450024322885));
#29564=CARTESIAN_POINT('Ctrl Pts',(-2.92350431159035,-0.368291087083228,
2.34212073872434));
#29565=CARTESIAN_POINT('Ctrl Pts',(-2.93879736301763,-0.246894422727957,
2.33547253151276));
#29566=CARTESIAN_POINT('Ctrl Pts',(-2.94579921760659,-0.124453265927633,
2.32882432430118));
#29567=CARTESIAN_POINT('Ctrl Pts',(-2.94487182720719,-0.00190539986535287,
2.32217611708959));
#29568=CARTESIAN_POINT('Ctrl Pts',(-2.94409804542743,-0.00221960462873976,
2.1778238829104));
#29569=CARTESIAN_POINT('Ctrl Pts',(-2.94538405566721,-0.155139230593375,
2.18611406173884));
#29570=CARTESIAN_POINT('Ctrl Pts',(-2.93447780370748,-0.307875103637501,
2.19440424056728));
#29571=CARTESIAN_POINT('Ctrl Pts',(-2.91073286453113,-0.458588216909009,
2.20269441939573));
#29572=CARTESIAN_POINT('Ctrl Pts',(-2.76051827213159,-1.41202544036162,
2.25513952461944));
#29573=CARTESIAN_POINT('Ctrl Pts',(-2.09649345438802,-2.28451087824219,
2.30758462984315));
#29574=CARTESIAN_POINT('Ctrl Pts',(-1.21754466145652,-2.68332862013697,
2.36002973506685));
#29575=CARTESIAN_POINT('Ctrl Pts',(-0.338595868525027,-3.08214636203174,
2.41247484029056));
#29576=CARTESIAN_POINT('Ctrl Pts',(0.755276899594388,-3.00729640794073,
2.46491994551426));
#29577=CARTESIAN_POINT('Ctrl Pts',(1.57170784623814,-2.49246924635079,2.51736505073797));
#29578=CARTESIAN_POINT('Ctrl Pts',(2.3881387928819,-1.97764208476085,2.56981015596168));
#29579=CARTESIAN_POINT('Ctrl Pts',(2.92712791805,-1.02283771567197,2.62225526118539));
#29580=CARTESIAN_POINT('Ctrl Pts',(2.94606932856971,-0.0578258660348382,
2.6747003664091));
#29581=CARTESIAN_POINT('Ctrl Pts',(2.96501073908941,0.907185983602299,2.72714547163281));
#29582=CARTESIAN_POINT('Ctrl Pts',(2.46390443496074,1.88240531378769,2.77959057685651));
#29583=CARTESIAN_POINT('Ctrl Pts',(1.66830473495772,2.42887370127543,2.83203568208022));
#29584=CARTESIAN_POINT('Ctrl Pts',(0.872705034954712,2.97534208876317,2.88448078730393));
#29585=CARTESIAN_POINT('Ctrl Pts',(-0.217388060922636,3.09305953355326,
2.93692589252764));
#29586=CARTESIAN_POINT('Ctrl Pts',(-1.11130990317228,2.72903986659667,2.98937099775135));
#29587=CARTESIAN_POINT('Ctrl Pts',(-2.00523174542191,2.36502019964009,3.04181610297505));
#29588=CARTESIAN_POINT('Ctrl Pts',(-2.70298233404385,1.51926342093683,3.09426120819876));
#29589=CARTESIAN_POINT('Ctrl Pts',(-2.89049530439613,0.572455370821353,
3.14670631342247));
#29590=CARTESIAN_POINT('Ctrl Pts',(-2.92758137029262,0.385196933861252,
3.15707883658511));
#29591=CARTESIAN_POINT('Ctrl Pts',(-2.94470877622731,0.1939857347123,3.16745135974775));
#29592=CARTESIAN_POINT('Ctrl Pts',(-2.94300132914192,0.00247067809074119,
3.17782388291039));
#29593=CARTESIAN_POINT('Origin',(0.,0.,0.));
#29594=CARTESIAN_POINT('',(-2.93815144027097,-0.00144838940242836,4.32217611708959));
#29595=CARTESIAN_POINT('',(-2.93758805006728,-0.000810565913221897,4.1778238829104));
#29596=CARTESIAN_POINT('',(-2.942,-3.60291088309151E-16,0.));
#29597=CARTESIAN_POINT('Ctrl Pts',(-2.93815144027097,-0.00144838940242836,
4.32217611708959));
#29598=CARTESIAN_POINT('Ctrl Pts',(-2.93549507201127,0.581944663119171,
4.29071171168856));
#29599=CARTESIAN_POINT('Ctrl Pts',(-2.76704590305946,1.16675179323199,4.25924730628754));
#29600=CARTESIAN_POINT('Ctrl Pts',(-2.44338137442995,1.64693751569171,4.22778290088651));
#29601=CARTESIAN_POINT('Ctrl Pts',(-1.90456974207211,2.44631350554451,4.175403396382));
#29602=CARTESIAN_POINT('Ctrl Pts',(-0.93560961338887,2.95575207374732,4.1230238918775));
#29603=CARTESIAN_POINT('Ctrl Pts',(0.0283581627927666,2.94647442485208,
4.07064438737299));
#29604=CARTESIAN_POINT('Ctrl Pts',(0.992325938974403,2.93719677595684,4.01826488286848));
#29605=CARTESIAN_POINT('Ctrl Pts',(1.95130136265442,2.40920290996356,3.96588537836398));
#29606=CARTESIAN_POINT('Ctrl Pts',(2.4746275187937,1.59960444002515,3.91350587385948));
#29607=CARTESIAN_POINT('Ctrl Pts',(2.99795367493297,0.790005970086747,3.86112636935497));
#29608=CARTESIAN_POINT('Ctrl Pts',(3.0856305635315,-0.301197103796779,3.80874686485047));
#29609=CARTESIAN_POINT('Ctrl Pts',(2.69828422619929,-1.18396704178881,3.75636736034596));
#29610=CARTESIAN_POINT('Ctrl Pts',(2.31093788886708,-2.06673697978085,3.70398785584146));
#29611=CARTESIAN_POINT('Ctrl Pts',(1.44856832560414,-2.7410737818814,3.65160835133695));
#29612=CARTESIAN_POINT('Ctrl Pts',(0.498448668458934,-2.90414611332682,
3.59922884683245));
#29613=CARTESIAN_POINT('Ctrl Pts',(-0.451670988686273,-3.06721844477224,
3.54684934232795));
#29614=CARTESIAN_POINT('Ctrl Pts',(-1.48954073971375,-2.71902630556253,
3.49446983782344));
#29615=CARTESIAN_POINT('Ctrl Pts',(-2.1490737861909,-2.01593590702758,3.44209033331894));
#29616=CARTESIAN_POINT('Ctrl Pts',(-2.65237107835254,-1.47939949597489,
3.40211892790916));
#29617=CARTESIAN_POINT('Ctrl Pts',(-2.93534805643284,-0.736191897535303,
3.36214752249938));
#29618=CARTESIAN_POINT('Ctrl Pts',(-2.94188729812012,0.00254759896953657,
3.32217611708959));
#29619=CARTESIAN_POINT('Ctrl Pts',(-2.94300132914192,0.00247067809074119,
3.17782388291039));
#29620=CARTESIAN_POINT('Ctrl Pts',(-2.93607565575577,-0.774344452547842,
3.21989646497146));
#29621=CARTESIAN_POINT('Ctrl Pts',(-2.61927127105561,-1.55615877069983,
3.26196904703253));
#29622=CARTESIAN_POINT('Ctrl Pts',(-2.06758380697847,-2.0994678941542,3.30404162909359));
#29623=CARTESIAN_POINT('Ctrl Pts',(-1.37988398712591,-2.77672378748653,
3.3564867343173));
#29624=CARTESIAN_POINT('Ctrl Pts',(-0.327208995338195,-3.08337625262348,
3.40893183954101));
#29625=CARTESIAN_POINT('Ctrl Pts',(0.616618861412321,-2.88139713307019,
3.46137694476472));
#29626=CARTESIAN_POINT('Ctrl Pts',(1.56044671816283,-2.67941801351691,3.51382204998842));
#29627=CARTESIAN_POINT('Ctrl Pts',(2.39542743987614,-1.9688073092734,3.56626715521213));
#29628=CARTESIAN_POINT('Ctrl Pts',(2.74572565546219,-1.06941987852551,3.61871226043584));
#29629=CARTESIAN_POINT('Ctrl Pts',(3.09602387104824,-0.170032447777603,
3.67115736565955));
#29630=CARTESIAN_POINT('Ctrl Pts',(2.96163958050702,0.918131709474696,3.72360247088326));
#29631=CARTESIAN_POINT('Ctrl Pts',(2.40306085127007,1.70527616384954,3.77604757610696));
#29632=CARTESIAN_POINT('Ctrl Pts',(1.84448212203313,2.49242061822439,3.82849268133067));
#29633=CARTESIAN_POINT('Ctrl Pts',(0.86170895410048,2.97854536972178,3.88093778655438));
#29634=CARTESIAN_POINT('Ctrl Pts',(-0.10290003671811,2.94483952623603,3.93338289177809));
#29635=CARTESIAN_POINT('Ctrl Pts',(-1.06750902753671,2.91113368275028,3.98582799700179));
#29636=CARTESIAN_POINT('Ctrl Pts',(-2.01395384124124,2.35759724428137,4.0382731022255));
#29637=CARTESIAN_POINT('Ctrl Pts',(-2.51622771244025,1.53338395412712,4.09071820744921));
#29638=CARTESIAN_POINT('Ctrl Pts',(-2.79430199366995,1.07707409733029,4.11975343260294));
#29639=CARTESIAN_POINT('Ctrl Pts',(-2.9362347477918,0.537799876108109,4.14878865775667));
#29640=CARTESIAN_POINT('Ctrl Pts',(-2.93758805006728,-0.000810565913221897,
4.1778238829104));
#29641=CARTESIAN_POINT('Origin',(0.,0.,0.));
#29642=CARTESIAN_POINT('',(-2.94644869531747,-0.000604754645607275,5.3221761170896));
#29643=CARTESIAN_POINT('',(-2.945679792052,-0.00146169071580815,5.1778238829104));
#29644=CARTESIAN_POINT('',(-2.942,-3.60291088309151E-16,0.));
#29645=CARTESIAN_POINT('Ctrl Pts',(-2.94644869531747,-0.000604754645607275,
5.3221761170896));
#29646=CARTESIAN_POINT('Ctrl Pts',(-2.94379550054715,0.929335583914262,
5.27165540538226));
#29647=CARTESIAN_POINT('Ctrl Pts',(-2.46604729438678,1.86162808593007,5.22113469367492));
#29648=CARTESIAN_POINT('Ctrl Pts',(-1.70849336410036,2.40074283220066,5.17061398196758));
#29649=CARTESIAN_POINT('Ctrl Pts',(-0.923066988207087,2.95969305927406,
5.11823447746308));
#29650=CARTESIAN_POINT('Ctrl Pts',(0.163133494924937,3.09600115191732,5.06585497295858));
#29651=CARTESIAN_POINT('Ctrl Pts',(1.06231690977038,2.74845383893534,5.01347546845407));
#29652=CARTESIAN_POINT('Ctrl Pts',(1.96150032461582,2.40090652595338,4.96109596394957));
#29653=CARTESIAN_POINT('Ctrl Pts',(2.67366667117468,1.56950380734618,4.90871645944506));
#29654=CARTESIAN_POINT('Ctrl Pts',(2.87899611438783,0.627612216959094,4.85633695494056));
#29655=CARTESIAN_POINT('Ctrl Pts',(3.08432555760098,-0.314279373428012,
4.80395745043605));
#29656=CARTESIAN_POINT('Ctrl Pts',(2.7828180974684,-1.36665983559502,4.75157794593155));
#29657=CARTESIAN_POINT('Ctrl Pts',(2.10987477706647,-2.05692589721429,4.69919844142705));
#29658=CARTESIAN_POINT('Ctrl Pts',(1.43693145666455,-2.74719195883355,4.64681893692254));
#29659=CARTESIAN_POINT('Ctrl Pts',(0.392552275993288,-3.07534361990509,
4.59443943241804));
#29660=CARTESIAN_POINT('Ctrl Pts',(-0.554252710038128,-2.89401445313919,
4.54205992791353));
#29661=CARTESIAN_POINT('Ctrl Pts',(-1.50105769606954,-2.71268528637328,
4.48968042340903));
#29662=CARTESIAN_POINT('Ctrl Pts',(-2.35028848746111,-2.02187529176995,
4.43730091890452));
#29663=CARTESIAN_POINT('Ctrl Pts',(-2.72057231514067,-1.13181358871689,
4.38492141440002));
#29664=CARTESIAN_POINT('Ctrl Pts',(-2.86842638565151,-0.776412580180032,
4.36400631529654));
#29665=CARTESIAN_POINT('Ctrl Pts',(-2.93991718809614,-0.389242894153138,
4.34309121619307));
#29666=CARTESIAN_POINT('Ctrl Pts',(-2.93815144027097,-0.00144838940242836,
4.32217611708959));
#29667=CARTESIAN_POINT('Ctrl Pts',(-2.93758805006728,-0.000810565913221897,
4.1778238829104));
#29668=CARTESIAN_POINT('Ctrl Pts',(-2.93867916073716,-0.435069497448956,
4.20123376298038));
#29669=CARTESIAN_POINT('Ctrl Pts',(-2.84838634229403,-0.86889693810433,
4.22464364305035));
#29670=CARTESIAN_POINT('Ctrl Pts',(-2.66438363654231,-1.25846258937073,
4.24805352312033));
#29671=CARTESIAN_POINT('Ctrl Pts',(-2.25216276075188,-2.13120570087471,
4.30049862834404));
#29672=CARTESIAN_POINT('Ctrl Pts',(-1.36961808047753,-2.78180178204309,
4.35294373356775));
#29673=CARTESIAN_POINT('Ctrl Pts',(-0.413994103635433,-2.91740931891088,
4.40538883879146));
#29674=CARTESIAN_POINT('Ctrl Pts',(0.541629873206673,-3.05301685577867,
4.45783394401517));
#29675=CARTESIAN_POINT('Ctrl Pts',(1.57033314661653,-2.67363584834587,4.51027904923887));
#29676=CARTESIAN_POINT('Ctrl Pts',(2.20908337968645,-1.9500304800975,4.56272415446258));
#29677=CARTESIAN_POINT('Ctrl Pts',(2.84783361275636,-1.22642511184914,4.61516925968629));
#29678=CARTESIAN_POINT('Ctrl Pts',(3.09663080548633,-0.158595382785209,
4.66761436491));
#29679=CARTESIAN_POINT('Ctrl Pts',(2.84348819889812,0.772815058373636,4.7200594701337));
#29680=CARTESIAN_POINT('Ctrl Pts',(2.5903455923099,1.70422549953248,4.77250457535741));
#29681=CARTESIAN_POINT('Ctrl Pts',(1.83526318640351,2.49921665278624,4.82494968058112));
#29682=CARTESIAN_POINT('Ctrl Pts',(0.918113109485756,2.79995295852677,4.87739478580482));
#29683=CARTESIAN_POINT('Ctrl Pts',(0.000963032567994487,3.1006892642673,
4.92983989102853));
#29684=CARTESIAN_POINT('Ctrl Pts',(-1.07825471536113,2.90717072249458,4.98228499625224));
#29685=CARTESIAN_POINT('Ctrl Pts',(-1.83377059439506,2.30650247319915,5.03473010147595));
#29686=CARTESIAN_POINT('Ctrl Pts',(-2.5208993779335,1.76020496324304,5.08242802862077));
#29687=CARTESIAN_POINT('Ctrl Pts',(-2.94027519175655,0.877129838501974,
5.13012595576559));
#29688=CARTESIAN_POINT('Ctrl Pts',(-2.945679792052,-0.00146169071580815,
5.1778238829104));
#29689=CARTESIAN_POINT('Origin',(0.,0.,0.));
#29690=CARTESIAN_POINT('',(-2.93949980478958,0.00219056232359141,6.3221761170896));
#29691=CARTESIAN_POINT('',(-2.94109090649655,0.00253660757586993,6.1778238829104));
#29692=CARTESIAN_POINT('',(-2.942,-3.60291088309151E-16,0.));
#29693=CARTESIAN_POINT('Ctrl Pts',(-2.93949980478958,0.00219056232359141,
6.3221761170896));
#29694=CARTESIAN_POINT('Ctrl Pts',(-2.94176361798241,0.320687415620876,
6.30497860358046));
#29695=CARTESIAN_POINT('Ctrl Pts',(-2.89395610782771,0.638523376129415,
6.28778109007132));
#29696=CARTESIAN_POINT('Ctrl Pts',(-2.79314214575126,0.938548174128603,
6.27058357656218));
#29697=CARTESIAN_POINT('Ctrl Pts',(-2.48608697885785,1.85235180335153,6.21820407205768));
#29698=CARTESIAN_POINT('Ctrl Pts',(-1.68730919078036,2.60092740470414,6.16582456755317));
#29699=CARTESIAN_POINT('Ctrl Pts',(-0.75552410366601,2.84810446618733,6.11344506304867));
#29700=CARTESIAN_POINT('Ctrl Pts',(0.176260983448343,3.09528152767051,6.06106555854416));
#29701=CARTESIAN_POINT('Ctrl Pts',(1.24105336959955,2.84106004928427,6.00868605403966));
#29702=CARTESIAN_POINT('Ctrl Pts',(1.96067583262663,2.19960587399116,5.95630654953515));
#29703=CARTESIAN_POINT('Ctrl Pts',(2.68029829565369,1.55815169869806,5.90392704503064));
#29704=CARTESIAN_POINT('Ctrl Pts',(3.05475083555665,0.52946482649812,5.85154754052614));
#29705=CARTESIAN_POINT('Ctrl Pts',(2.91587421520356,-0.424491793382225,
5.79916803602164));
#29706=CARTESIAN_POINT('Ctrl Pts',(2.77699759485047,-1.37844841326258,5.74678853151713));
#29707=CARTESIAN_POINT('Ctrl Pts',(2.12479181424134,-2.25767478082334,5.69440902701263));
#29708=CARTESIAN_POINT('Ctrl Pts',(1.25214960298458,-2.66732770639159,5.64202952250812));
#29709=CARTESIAN_POINT('Ctrl Pts',(0.379507391727844,-3.07698063195983,
5.58965001800362));
#29710=CARTESIAN_POINT('Ctrl Pts',(-0.713571250176501,-3.01706011553558,
5.53727051349912));
#29711=CARTESIAN_POINT('Ctrl Pts',(-1.53620630199898,-2.5144752771182,5.48489100899462));
#29712=CARTESIAN_POINT('Ctrl Pts',(-2.35884135382146,-2.01189043870081,
5.43251150449011));
#29713=CARTESIAN_POINT('Ctrl Pts',(-2.91103281556208,-1.0666412782903,5.3801319999856));
#29714=CARTESIAN_POINT('Ctrl Pts',(-2.94480241210512,-0.103220517333276,
5.3277524954811));
#29715=CARTESIAN_POINT('Ctrl Pts',(-2.94600079462919,-0.069031580495304,
5.32589370268393));
#29716=CARTESIAN_POINT('Ctrl Pts',(-2.94654631348559,-0.0348197596345374,
5.32403490988676));
#29717=CARTESIAN_POINT('Ctrl Pts',(-2.94644869531747,-0.000604754645607275,
5.3221761170896));
#29718=CARTESIAN_POINT('Ctrl Pts',(-2.945679792052,-0.00146169071580815,
5.1778238829104));
#29719=CARTESIAN_POINT('Ctrl Pts',(-2.94621768964176,-0.0889042840834332,
5.18257106098929));
#29720=CARTESIAN_POINT('Ctrl Pts',(-2.94265503660913,-0.176302465642187,
5.18731823906819));
#29721=CARTESIAN_POINT('Ctrl Pts',(-2.93484768462379,-0.263319805187537,
5.19206541714708));
#29722=CARTESIAN_POINT('Ctrl Pts',(-2.84859488567985,-1.22465587746066,
5.24451052237078));
#29723=CARTESIAN_POINT('Ctrl Pts',(-2.24427527765324,-2.13951006518879,
5.29695562759449));
#29724=CARTESIAN_POINT('Ctrl Pts',(-1.39390074925371,-2.59609494298297,
5.34940073281819));
#29725=CARTESIAN_POINT('Ctrl Pts',(-0.543526220854162,-3.05267982077716,
5.4018458380419));
#29726=CARTESIAN_POINT('Ctrl Pts',(0.552903227918311,-3.05099538863739,
5.45429094326562));
#29727=CARTESIAN_POINT('Ctrl Pts',(1.40187085321134,-2.59179983074767,5.50673604848932));
#29728=CARTESIAN_POINT('Ctrl Pts',(2.25083847850436,-2.13260427285796,5.55918115371303));
#29729=CARTESIAN_POINT('Ctrl Pts',(2.85234428031795,-1.21589758921833,5.61162625893673));
#29730=CARTESIAN_POINT('Ctrl Pts',(2.93564289965894,-0.254301037021637,
5.66407136416044));
#29731=CARTESIAN_POINT('Ctrl Pts',(3.01894151899992,0.707295515175046,5.71651646938415));
#29732=CARTESIAN_POINT('Ctrl Pts',(2.5840329558683,1.71378193592877,5.76896157460786));
#29733=CARTESIAN_POINT('Ctrl Pts',(1.82667504784324,2.31212597436553,5.82140667983157));
#29734=CARTESIAN_POINT('Ctrl Pts',(1.06931713981816,2.9104700128023,5.87385178505528));
#29735=CARTESIAN_POINT('Ctrl Pts',(-0.010490113100349,3.1006716689221,5.92629689027898));
#29736=CARTESIAN_POINT('Ctrl Pts',(-0.92671182736886,2.79711877487579,5.97874199550269));
#29737=CARTESIAN_POINT('Ctrl Pts',(-1.84293354163737,2.49356588082949,6.0311871007264));
#29738=CARTESIAN_POINT('Ctrl Pts',(-2.59556971725588,1.69625843661705,6.08363220595011));
#29739=CARTESIAN_POINT('Ctrl Pts',(-2.84584930505901,0.764074593638618,
6.13607731117382));
#29740=CARTESIAN_POINT('Ctrl Pts',(-2.91225724864025,0.516733559576513,
6.14999283508601));
#29741=CARTESIAN_POINT('Ctrl Pts',(-2.94329794130529,0.259896865352817,
6.16390835899821));
#29742=CARTESIAN_POINT('Ctrl Pts',(-2.94109090649655,0.00253660757586993,
6.1778238829104));
#29743=CARTESIAN_POINT('Origin',(0.,0.,0.));
#29744=CARTESIAN_POINT('',(-2.93998607517527,-0.0023358300504342,7.3221761170896));
#29745=CARTESIAN_POINT('',(-2.93846014819028,-0.00170708260597003,7.1778238829104));
#29746=CARTESIAN_POINT('',(-2.942,-3.60291088309151E-16,0.));
#29747=CARTESIAN_POINT('Ctrl Pts',(-2.93998607517527,-0.0023358300504342,
7.3221761170896));
#29748=CARTESIAN_POINT('Ctrl Pts',(-2.93483565594967,0.668801419715884,
7.28592229727415));
#29749=CARTESIAN_POINT('Ctrl Pts',(-2.70624449366069,1.34311250814063,7.2496684774587));
#29750=CARTESIAN_POINT('Ctrl Pts',(-2.28495024526271,1.86051554631288,7.21341465764326));
#29751=CARTESIAN_POINT('Ctrl Pts',(-1.67626448210673,2.60805925085354,7.16103515313876));
#29752=CARTESIAN_POINT('Ctrl Pts',(-0.665321452888303,3.02806588999372,
7.10865564863425));
#29753=CARTESIAN_POINT('Ctrl Pts',(0.293884302746592,2.93191878092119,7.05627614412975));
#29754=CARTESIAN_POINT('Ctrl Pts',(1.25309005838148,2.83577167184866,7.00389663962524));
#29755=CARTESIAN_POINT('Ctrl Pts',(2.16055854043283,2.22347081456344,6.95151713512074));
#29756=CARTESIAN_POINT('Ctrl Pts',(2.60876358347624,1.3699884259484,6.89913763061623));
#29757=CARTESIAN_POINT('Ctrl Pts',(3.05696862651966,0.516506037333356,6.84675812611173));
#29758=CARTESIAN_POINT('Ctrl Pts',(3.04591023055511,-0.578157882611513,
6.79437862160723));
#29759=CARTESIAN_POINT('Ctrl Pts',(2.58055450279311,-1.42241139605186,6.74199911710272));
#29760=CARTESIAN_POINT('Ctrl Pts',(2.11519877503111,-2.26666490949219,6.68961961259822));
#29761=CARTESIAN_POINT('Ctrl Pts',(1.19554571547167,-2.86050801642801,6.63724010809371));
#29762=CARTESIAN_POINT('Ctrl Pts',(0.234593342362696,-2.93725751088208,
6.5848606035892));
#29763=CARTESIAN_POINT('Ctrl Pts',(-0.726359030746288,-3.01400700533615,
6.5324810990847));
#29764=CARTESIAN_POINT('Ctrl Pts',(-1.72861071740481,-2.57366288730847,
6.4801015945802));
#29765=CARTESIAN_POINT('Ctrl Pts',(-2.32207028787941,-1.813974999748,6.4277220900757));
#29766=CARTESIAN_POINT('Ctrl Pts',(-2.72068210106971,-1.30371182195979,
6.39254009908033));
#29767=CARTESIAN_POINT('Ctrl Pts',(-2.93486858555413,-0.649377666932483,
6.35735810808496));
#29768=CARTESIAN_POINT('Ctrl Pts',(-2.93949980478958,0.00219056232359141,
6.3221761170896));
#29769=CARTESIAN_POINT('Ctrl Pts',(-2.94109090649655,0.00253660757586993,
6.1778238829104));
#29770=CARTESIAN_POINT('Ctrl Pts',(-2.9349800243151,-0.710047628629508,
6.21635346422191));
#29771=CARTESIAN_POINT('Ctrl Pts',(-2.67397994955092,-1.42664569379386,
6.25488304553342));
#29772=CARTESIAN_POINT('Ctrl Pts',(-2.20308134670334,-1.95680883878727,
6.29341262684494));
#29773=CARTESIAN_POINT('Ctrl Pts',(-1.5621108005568,-2.67844818649031,6.34585773206864));
#29774=CARTESIAN_POINT('Ctrl Pts',(-0.532246708275948,-3.05466664015197,
6.39830283729235));
#29775=CARTESIAN_POINT('Ctrl Pts',(0.42295609402977,-2.91612352177857,6.45074794251606));
#29776=CARTESIAN_POINT('Ctrl Pts',(1.3781588963355,-2.77758040340517,6.50319304773977));
#29777=CARTESIAN_POINT('Ctrl Pts',(2.25870040866608,-2.12427571299673,6.55563815296348));
#29778=CARTESIAN_POINT('Ctrl Pts',(2.66823777423309,-1.25027014357196,6.60808325818718));
#29779=CARTESIAN_POINT('Ctrl Pts',(3.07777513980009,-0.376264574147203,
6.66052836341089));
#29780=CARTESIAN_POINT('Ctrl Pts',(3.01630835860352,0.718441874293864,6.7129734686346));
#29781=CARTESIAN_POINT('Ctrl Pts',(2.51150440524776,1.54110800210975,6.76541857385831));
#29782=CARTESIAN_POINT('Ctrl Pts',(2.006700451892,2.36377412992563,6.81786367908202));
#29783=CARTESIAN_POINT('Ctrl Pts',(1.05855932637705,2.91439993711633,6.87030878430572));
#29784=CARTESIAN_POINT('Ctrl Pts',(0.0938513252260113,2.94514179293546,
6.92275388952943));
#29785=CARTESIAN_POINT('Ctrl Pts',(-0.870856675925038,2.9758836487546,6.97519899475314));
#29786=CARTESIAN_POINT('Ctrl Pts',(-1.85213155271217,2.48674155320215,7.02764409997685));
#29787=CARTESIAN_POINT('Ctrl Pts',(-2.40828908863565,1.69788454181399,7.08008920520056));
#29788=CARTESIAN_POINT('Ctrl Pts',(-2.75376700818296,1.2078566962645,7.11266743110384));
#29789=CARTESIAN_POINT('Ctrl Pts',(-2.93520341737875,0.60217681128353,7.14524565700712));
#29790=CARTESIAN_POINT('Ctrl Pts',(-2.93846014819028,-0.00170708260597003,
7.1778238829104));
#29791=CARTESIAN_POINT('Origin',(0.,0.,0.));
#29792=CARTESIAN_POINT('',(-2.94622250669394,0.000937675328142526,8.3221761170896));
#29793=CARTESIAN_POINT('',(-2.94656696235233,-0.000396508504380587,8.1778238829104));
#29794=CARTESIAN_POINT('',(-2.942,-3.60291088309151E-16,0.));
#29795=CARTESIAN_POINT('Ctrl Pts',(-2.94622250669394,0.000937675328142526,
8.3221761170896));
#29796=CARTESIAN_POINT('Ctrl Pts',(-2.94645073222768,0.0548930361868928,
8.31924549547236));
#29797=CARTESIAN_POINT('Ctrl Pts',(-2.94509413407217,0.108836699779164,
8.31631487385511));
#29798=CARTESIAN_POINT('Ctrl Pts',(-2.94211616003438,0.162690705921765,
8.31338425223786));
#29799=CARTESIAN_POINT('Ctrl Pts',(-2.88889031756852,1.12523262560549,8.26100474773336));
#29800=CARTESIAN_POINT('Ctrl Pts',(-2.31771549444688,2.05913344782865,8.20862524322884));
#29801=CARTESIAN_POINT('Ctrl Pts',(-1.48509504480843,2.54499674522788,8.15624573872434));
#29802=CARTESIAN_POINT('Ctrl Pts',(-0.652474595169965,3.03086004262711,
8.10386623421983));
#29803=CARTESIAN_POINT('Ctrl Pts',(0.44159148098532,3.06868581520241,8.05148672971533));
#29804=CARTESIAN_POINT('Ctrl Pts',(1.30577973958019,2.64148726651903,7.99910722521083));
#29805=CARTESIAN_POINT('Ctrl Pts',(2.16996799817506,2.21428871783565,7.94672772070633));
#29806=CARTESIAN_POINT('Ctrl Pts',(2.8042784392095,1.3220658478936,7.89434821620182));
#29807=CARTESIAN_POINT('Ctrl Pts',(2.92385476924452,0.36549831322338,7.84196871169732));
#29808=CARTESIAN_POINT('Ctrl Pts',(3.04343109927954,-0.591069221446826,
7.78958920719281));
#29809=CARTESIAN_POINT('Ctrl Pts',(2.64827331831513,-1.61198142084519,7.73720970268831));
#29810=CARTESIAN_POINT('Ctrl Pts',(1.9158389819387,-2.23876678477201,7.68483019818381));
#29811=CARTESIAN_POINT('Ctrl Pts',(1.18340464556226,-2.86555214869884,7.6324506936793));
#29812=CARTESIAN_POINT('Ctrl Pts',(0.113693753773775,-3.09821067715411,
7.58007118917479));
#29813=CARTESIAN_POINT('Ctrl Pts',(-0.812907669552306,-2.83226002346519,
7.52769168467029));
#29814=CARTESIAN_POINT('Ctrl Pts',(-1.73950909287838,-2.56630936977627,
7.47531218016578));
#29815=CARTESIAN_POINT('Ctrl Pts',(-2.52300104774206,-1.80174953394315,
7.42293267566128));
#29816=CARTESIAN_POINT('Ctrl Pts',(-2.81153277662714,-0.881929231056029,
7.37055317115678));
#29817=CARTESIAN_POINT('Ctrl Pts',(-2.90036087316611,-0.598751062127826,
7.35442748646772));
#29818=CARTESIAN_POINT('Ctrl Pts',(-2.94227697960606,-0.300857412821767,
7.33830180177866));
#29819=CARTESIAN_POINT('Ctrl Pts',(-2.93998607517527,-0.0023358300504342,
7.3221761170896));
#29820=CARTESIAN_POINT('Ctrl Pts',(-2.93846014819028,-0.00170708260597003,
7.1778238829104));
#29821=CARTESIAN_POINT('Ctrl Pts',(-2.94044617033292,-0.369968033311824,
7.19769076223082));
#29822=CARTESIAN_POINT('Ctrl Pts',(-2.87617048586605,-0.737561088352721,
7.21755764155125));
#29823=CARTESIAN_POINT('Ctrl Pts',(-2.7424268268773,-1.07785126568817,7.23742452087168));
#29824=CARTESIAN_POINT('Ctrl Pts',(-2.38936683413567,-1.97615813457835,
7.28986962609539));
#29825=CARTESIAN_POINT('Ctrl Pts',(-1.55220665359259,-2.68419994513487,
7.34231473131909));
#29826=CARTESIAN_POINT('Ctrl Pts',(-0.60776265660645,-2.88327813520494,
7.3947598365428));
#29827=CARTESIAN_POINT('Ctrl Pts',(0.336681340379679,-3.082356325275,7.44720494176651));
#29828=CARTESIAN_POINT('Ctrl Pts',(1.38840915380886,-2.77247089485864,7.49965004699022));
#29829=CARTESIAN_POINT('Ctrl Pts',(2.07402481044015,-2.09310519028348,7.55209515221392));
#29830=CARTESIAN_POINT('Ctrl Pts',(2.75964046707144,-1.41373948570832,7.60454025743763));
#29831=CARTESIAN_POINT('Ctrl Pts',(3.07914396690482,-0.364893506974353,
7.65698536266134));
#29832=CARTESIAN_POINT('Ctrl Pts',(2.8887227491853,0.5813339228528,7.70943046788505));
#29833=CARTESIAN_POINT('Ctrl Pts',(2.69830153146578,1.52756135267996,7.76187557310876));
#29834=CARTESIAN_POINT('Ctrl Pts',(1.99795559619334,2.37117023360031,7.81432067833246));
#29835=CARTESIAN_POINT('Ctrl Pts',(1.10291949457769,2.73244155291697,7.86676578355617));
#29836=CARTESIAN_POINT('Ctrl Pts',(0.207883392962048,3.09371287223363,7.91921088877988));
#29837=CARTESIAN_POINT('Ctrl Pts',(-0.881842874996807,2.97264662994661,
7.97165599400359));
#29838=CARTESIAN_POINT('Ctrl Pts',(-1.67575975122609,2.42373627051487,8.0241010992273));
#29839=CARTESIAN_POINT('Ctrl Pts',(-2.45144772506959,1.88742928765845,8.07534202712166));
#29840=CARTESIAN_POINT('Ctrl Pts',(-2.94475435076587,0.942699847726619,
8.12658295501603));
#29841=CARTESIAN_POINT('Ctrl Pts',(-2.94656696235233,-0.000396508504380587,
8.1778238829104));
#29842=CARTESIAN_POINT('Origin',(0.,0.,0.));
#29843=CARTESIAN_POINT('',(-2.93787859032851,0.00118007037484616,9.3221761170896));
#29844=CARTESIAN_POINT('',(-2.93938212312892,0.00216771032458683,9.1778238829104));
#29845=CARTESIAN_POINT('',(-2.942,-3.60291088309151E-16,0.));
#29846=CARTESIAN_POINT('Ctrl Pts',(-2.93787859032851,0.00118007037484616,
9.3221761170896));
#29847=CARTESIAN_POINT('Ctrl Pts',(-2.93938225399168,0.408942454113454,
9.30018918916604));
#29848=CARTESIAN_POINT('Ctrl Pts',(-2.86009946358647,0.816145924853212,
9.27820226124249));
#29849=CARTESIAN_POINT('Ctrl Pts',(-2.69715242952518,1.18654365111784,9.25621533331894));
#29850=CARTESIAN_POINT('Ctrl Pts',(-2.30896336853928,2.06894293121702,9.20383582881443));
#29851=CARTESIAN_POINT('Ctrl Pts',(-1.44594933104186,2.74245624053358,9.15145632430993));
#29852=CARTESIAN_POINT('Ctrl Pts',(-0.495674163844965,2.9046210644708,9.09907681980542));
#29853=CARTESIAN_POINT('Ctrl Pts',(0.454601003351916,3.06678588840801,9.04669731530092));
#29854=CARTESIAN_POINT('Ctrl Pts',(1.49213730024827,2.7176022269659,8.99431781079641));
#29855=CARTESIAN_POINT('Ctrl Pts',(2.15099835280526,2.01388208359571,8.94193830629191));
#29856=CARTESIAN_POINT('Ctrl Pts',(2.80985940536224,1.31016194022553,8.88955880178741));
#29857=CARTESIAN_POINT('Ctrl Pts',(3.09004521357986,0.251905314927287,8.8371792972829));
#29858=CARTESIAN_POINT('Ctrl Pts',(2.86572951288042,-0.685645923387644,
8.7847997927784));
#29859=CARTESIAN_POINT('Ctrl Pts',(2.64141381218099,-1.62319716170258,8.73242028827389));
#29860=CARTESIAN_POINT('Ctrl Pts',(1.91259660256449,-2.44004301303419,8.68004078376939));
#29861=CARTESIAN_POINT('Ctrl Pts',(1.00657547791151,-2.76935400264746,8.62766127926488));
#29862=CARTESIAN_POINT('Ctrl Pts',(0.100554353258536,-3.09866499226073,
8.57528177476038));
#29863=CARTESIAN_POINT('Ctrl Pts',(-0.982670686430926,-2.94044112015566,
8.52290227025587));
#29864=CARTESIAN_POINT('Ctrl Pts',(-1.75664477537062,-2.36573767553097,
8.47052276575137));
#29865=CARTESIAN_POINT('Ctrl Pts',(-2.48731518632227,-1.82318876070292,
8.42107388286411));
#29866=CARTESIAN_POINT('Ctrl Pts',(-2.94237161798714,-0.909460413780999,
8.37162499997686));
#29867=CARTESIAN_POINT('Ctrl Pts',(-2.94622250669394,0.000937675328142526,
8.3221761170896));
#29868=CARTESIAN_POINT('Ctrl Pts',(-2.94656696235233,-0.000396508504380587,
8.1778238829104));
#29869=CARTESIAN_POINT('Ctrl Pts',(-2.94660955927376,-0.0225595585939061,
8.17902806023974));
#29870=CARTESIAN_POINT('Ctrl Pts',(-2.94638072162746,-0.0447217067897041,
8.18023223756908));
#29871=CARTESIAN_POINT('Ctrl Pts',(-2.94587773547044,-0.0668776312364038,
8.18143641489842));
#29872=CARTESIAN_POINT('Ctrl Pts',(-2.92397135898579,-1.03182669697942,
8.23388152012213));
#29873=CARTESIAN_POINT('Ctrl Pts',(-2.3820511215168,-1.98497035188899,8.28632662534583));
#29874=CARTESIAN_POINT('Ctrl Pts',(-1.5640421648278,-2.49728659914907,8.33877173056954));
#29875=CARTESIAN_POINT('Ctrl Pts',(-0.746033208138801,-3.00960284640916,
8.39121683579325));
#29876=CARTESIAN_POINT('Ctrl Pts',(0.348064467770205,-3.08109168601973,
8.44366194101695));
#29877=CARTESIAN_POINT('Ctrl Pts',(1.22578367546087,-2.6795750856597,8.49610704624066));
#29878=CARTESIAN_POINT('Ctrl Pts',(2.10350288315153,-2.27805848529968,8.54855215146437));
#29879=CARTESIAN_POINT('Ctrl Pts',(2.76484362262384,-1.40353644496905,8.60099725668809));
#29880=CARTESIAN_POINT('Ctrl Pts',(2.91212808132915,-0.44964238612263,8.65344236191179));
#29881=CARTESIAN_POINT('Ctrl Pts',(3.05941254003446,0.504251672723784,8.7058874671355));
#29882=CARTESIAN_POINT('Ctrl Pts',(2.69264071797276,1.537517750086,8.75833257235921));
#29883=CARTESIAN_POINT('Ctrl Pts',(1.97690123029279,2.18506974304829,8.81077767758291));
#29884=CARTESIAN_POINT('Ctrl Pts',(1.26116174261282,2.83262173601059,8.86322278280662));
#29885=CARTESIAN_POINT('Ctrl Pts',(0.196454589314577,3.09445964457298,8.91566788803033));
#29886=CARTESIAN_POINT('Ctrl Pts',(-0.737982063629216,2.8527269003752,8.96811299325404));
#29887=CARTESIAN_POINT('Ctrl Pts',(-1.672418716573,2.61099415617743,9.02055809847774));
#29888=CARTESIAN_POINT('Ctrl Pts',(-2.47658486916233,1.86569075921951,9.07300320370145));
#29889=CARTESIAN_POINT('Ctrl Pts',(-2.78851523225651,0.952287217651892,
9.12544830892515));
#29890=CARTESIAN_POINT('Ctrl Pts',(-2.89235416848512,0.648223031136026,
9.1429068335869));
#29891=CARTESIAN_POINT('Ctrl Pts',(-2.94164516567622,0.325530543639097,
9.16036535824865));
#29892=CARTESIAN_POINT('Ctrl Pts',(-2.93938212312892,0.00216771032458683,
9.1778238829104));
#29893=CARTESIAN_POINT('Origin',(0.,0.,0.));
#29894=CARTESIAN_POINT('',(-2.94242444587263,-0.00248500551853048,10.3221761170896));
#29895=CARTESIAN_POINT('',(-2.93989309841074,-0.00232834448912937,10.1778238829104));
#29896=CARTESIAN_POINT('',(-2.942,-3.60291088309151E-16,0.));
#29897=CARTESIAN_POINT('Ctrl Pts',(-2.94242444587263,-0.00248500551853048,
10.3221761170896));
#29898=CARTESIAN_POINT('Ctrl Pts',(-2.93565996783783,0.755676872330999,
10.2811328828597));
#29899=CARTESIAN_POINT('Ctrl Pts',(-2.63573211439715,1.5185652175411,10.2400896486299));
#29900=CARTESIAN_POINT('Ctrl Pts',(-2.10792737213773,2.05892622612073,10.1990464144));
#29901=CARTESIAN_POINT('Ctrl Pts',(-1.43434130141424,2.74853664338077,10.1466669098955));
#29902=CARTESIAN_POINT('Ctrl Pts',(-0.389613404070186,3.07571802003838,
10.094287405391));
#29903=CARTESIAN_POINT('Ctrl Pts',(0.557026464387836,2.89349108573471,10.0419079008865));
#29904=CARTESIAN_POINT('Ctrl Pts',(1.50366633284582,2.71126415143105,9.98952839638201));
#29905=CARTESIAN_POINT('Ctrl Pts',(2.35221817241779,2.01962890616612,9.9371488918775));
#29906=CARTESIAN_POINT('Ctrl Pts',(2.72164717416933,1.12921048240304,9.884769387373));
#29907=CARTESIAN_POINT('Ctrl Pts',(3.09107617592089,0.238792058639911,9.83238988286849));
#29908=CARTESIAN_POINT('Ctrl Pts',(2.981382339852,-0.85040954362138,9.78001037836398));
#29909=CARTESIAN_POINT('Ctrl Pts',(2.44180970997212,-1.64926869616342,9.72763087385948));
#29910=CARTESIAN_POINT('Ctrl Pts',(1.90223708009224,-2.44812784870545,9.67525136935497));
#29911=CARTESIAN_POINT('Ctrl Pts',(0.93278565640137,-2.95664455152821,9.62287186485046));
#29912=CARTESIAN_POINT('Ctrl Pts',(-0.031174037472469,-2.94644704900523,
9.57049236034596));
#29913=CARTESIAN_POINT('Ctrl Pts',(-0.995133731346301,-2.93624954648225,
9.51811285584146));
#29914=CARTESIAN_POINT('Ctrl Pts',(-1.9536016954031,-2.40733783861356,9.46573335133695));
#29915=CARTESIAN_POINT('Ctrl Pts',(-2.4761536351943,-1.5972393592383,9.41335384683245));
#29916=CARTESIAN_POINT('Ctrl Pts',(-2.77935810415337,-1.1271894741653,9.3829612702515));
#29917=CARTESIAN_POINT('Ctrl Pts',(-2.93580007289335,-0.56247072784923,
9.35256869367055));
#29918=CARTESIAN_POINT('Ctrl Pts',(-2.93787859032851,0.00118007037484616,
9.3221761170896));
#29919=CARTESIAN_POINT('Ctrl Pts',(-2.93938212312892,0.00216771032458683,
9.1778238829104));
#29920=CARTESIAN_POINT('Ctrl Pts',(-2.93484702512206,-0.645845798130107,
9.21281046347236));
#29921=CARTESIAN_POINT('Ctrl Pts',(-2.72327366311651,-1.29655137950586,
9.24779704403432));
#29922=CARTESIAN_POINT('Ctrl Pts',(-2.32875660055073,-1.80542543875765,
9.28278362459629));
#29923=CARTESIAN_POINT('Ctrl Pts',(-1.73737303215174,-2.56823086742229,
9.33522872981999));
#29924=CARTESIAN_POINT('Ctrl Pts',(-0.73491132175476,-3.01233803857425,
9.3876738350437));
#29925=CARTESIAN_POINT('Ctrl Pts',(0.227407657021308,-2.93784857599215,
9.44011894026741));
#29926=CARTESIAN_POINT('Ctrl Pts',(1.1897266357974,-2.86335911341005,9.49256404549111));
#29927=CARTESIAN_POINT('Ctrl Pts',(2.11190288295256,-2.27027301709385,9.54500915071482));
#29928=CARTESIAN_POINT('Ctrl Pts',(2.57885359588429,-1.42554607687093,9.59745425593853));
#29929=CARTESIAN_POINT('Ctrl Pts',(3.045804308816,-0.580819136648041,9.64989936116224));
#29930=CARTESIAN_POINT('Ctrl Pts',(3.05752948752431,0.515548647481566,9.70234446638595));
#29931=CARTESIAN_POINT('Ctrl Pts',(2.60875076544854,1.37006875926759,9.75478957160966));
#29932=CARTESIAN_POINT('Ctrl Pts',(2.15997204337277,2.22458887105361,9.80723467683336));
#29933=CARTESIAN_POINT('Ctrl Pts',(1.25068942051291,2.83726131049606,9.85967978205706));
#29934=CARTESIAN_POINT('Ctrl Pts',(0.290183858659324,2.93231357229399,9.91212488728077));
#29935=CARTESIAN_POINT('Ctrl Pts',(-0.67032170319427,3.02736583409193,9.96456999250448));
#29936=CARTESIAN_POINT('Ctrl Pts',(-1.68205020404159,2.60479791824536,10.0170150977282));
#29937=CARTESIAN_POINT('Ctrl Pts',(-2.28961248249041,1.85481470515708,10.0694602029519));
#29938=CARTESIAN_POINT('Ctrl Pts',(-2.708067067946,1.33826862311137,10.1055814296047));
#29939=CARTESIAN_POINT('Ctrl Pts',(-2.93479827488144,0.666407318052135,
10.1417026562576));
#29940=CARTESIAN_POINT('Ctrl Pts',(-2.93989309841074,-0.00232834448912937,
10.1778238829104));
#29941=CARTESIAN_POINT('Origin',(0.,0.,-1.84858989190501));
#29942=CARTESIAN_POINT('',(-2.3720921752204,-0.00200333509135781,10.651410108095));
#29943=CARTESIAN_POINT('',(-2.37533330856671,0.000645282184899808,10.848589891905));
#29944=CARTESIAN_POINT('',(-2.37175,-1.78696459712734E-13,-1.84858989190501));
#29945=CARTESIAN_POINT('',(-2.34668236863852,0.343918483395543,11.62825));
#29946=CARTESIAN_POINT('Ctrl Pts',(-2.3720921752204,-0.00200333509135741,
10.651410108095));
#29947=CARTESIAN_POINT('Ctrl Pts',(-2.37359839777753,-0.170820576644891,
10.6627463783696));
#29948=CARTESIAN_POINT('Ctrl Pts',(-2.28072670946568,-1.11802807678178,
10.7264621531488));
#29949=CARTESIAN_POINT('Ctrl Pts',(-1.0098707589218,-2.60498459805753,10.8425574324324));
#29950=CARTESIAN_POINT('Ctrl Pts',(1.61803174729613,-2.2773674076414,10.999695945946));
#29951=CARTESIAN_POINT('Ctrl Pts',(2.79127527466209,0.0946110570183949,
11.1568344594594));
#29952=CARTESIAN_POINT('Ctrl Pts',(1.46022534703361,2.38369320998594,11.313972972973));
#29953=CARTESIAN_POINT('Ctrl Pts',(-1.1878082887304,2.52773050943662,11.4711114864865));
#29954=CARTESIAN_POINT('Ctrl Pts',(-2.23349531079268,1.11623543008163,11.5758704954955));
#29955=CARTESIAN_POINT('Ctrl Pts',(-2.34668236863853,0.343918483395475,
11.62825));
#29956=CARTESIAN_POINT('',(-0.439445221994028,2.33068358199191,11.62825));
#29957=CARTESIAN_POINT('Origin',(0.,0.,11.62825));
#29958=CARTESIAN_POINT('Ctrl Pts',(-2.37533330856671,0.000645282184899929,
10.848589891905));
#29959=CARTESIAN_POINT('Ctrl Pts',(-2.37266626526946,-0.74297942345447,
10.8986961737085));
#29960=CARTESIAN_POINT('Ctrl Pts',(-1.5987407489101,-2.26979394046941,11.0012475607357));
#29961=CARTESIAN_POINT('Ctrl Pts',(0.989622905930635,-2.61290295808564,
11.1562440529866));
#29962=CARTESIAN_POINT('Ctrl Pts',(2.72902843688469,-0.61088887604173,11.3135793686578));
#29963=CARTESIAN_POINT('Ctrl Pts',(2.00599839187704,1.9449087769569,11.4709146843289));
#29964=CARTESIAN_POINT('Ctrl Pts',(0.328567026486064,2.47549058867235,11.5758048947763));
#29965=CARTESIAN_POINT('Ctrl Pts',(-0.439445221994061,2.3306835819919,11.62825));
#29966=CARTESIAN_POINT('Origin',(0.,0.,-1.84858989190501));
#29967=CARTESIAN_POINT('',(-2.36842744616303,0.000951336475574988,9.65141010809499));
#29968=CARTESIAN_POINT('',(-2.37005148067835,-0.00187703978340947,9.84858989190503));
#29969=CARTESIAN_POINT('',(-2.37175,-1.78696459712734E-13,-1.84858989190501));
#29970=CARTESIAN_POINT('Ctrl Pts',(-2.36842744616303,0.000951336475575049,
9.65141010809499));
#29971=CARTESIAN_POINT('Ctrl Pts',(-2.36675180927421,-0.453446617531184,
9.68180268467594));
#29972=CARTESIAN_POINT('Ctrl Pts',(-2.02327622703562,-1.69331275929724,
9.76457476576139));
#29973=CARTESIAN_POINT('Ctrl Pts',(-0.0295588149451427,-2.79350652787453,
9.89972635135136));
#29974=CARTESIAN_POINT('Ctrl Pts',(2.31506703223917,-1.56365490661018,10.0568648648649));
#29975=CARTESIAN_POINT('Ctrl Pts',(2.58036243233743,1.07058768363104,10.2140033783784));
#29976=CARTESIAN_POINT('Ctrl Pts',(0.528133174514654,2.74331293137788,10.3711418918919));
#29977=CARTESIAN_POINT('Ctrl Pts',(-1.81626974066498,2.00910742659655,10.5169441351307));
#29978=CARTESIAN_POINT('Ctrl Pts',(-2.36663886088356,0.609203474490441,
10.6103668738651));
#29979=CARTESIAN_POINT('Ctrl Pts',(-2.3720921752204,-0.00200333509135741,
10.651410108095));
#29980=CARTESIAN_POINT('Ctrl Pts',(-2.37005148067835,-0.0018770397834093,
9.84858989190503));
#29981=CARTESIAN_POINT('Ctrl Pts',(-2.37190764427919,-0.245513112411714,
9.8649137704759));
#29982=CARTESIAN_POINT('Ctrl Pts',(-2.22599738542921,-1.26973141402768,
9.93368275427047));
#29983=CARTESIAN_POINT('Ctrl Pts',(-0.757654725048104,-2.69016151139635,
10.0548968432888));
#29984=CARTESIAN_POINT('Ctrl Pts',(1.83027666927001,-2.11210170665972,10.2122321589599));
#29985=CARTESIAN_POINT('Ctrl Pts',(2.77060484795253,0.367287133540841,10.369567474631));
#29986=CARTESIAN_POINT('Ctrl Pts',(1.21665350181368,2.51610800548609,10.5269027903021));
#29987=CARTESIAN_POINT('Ctrl Pts',(-1.43234772356642,2.39972494583597,10.6842381059733));
#29988=CARTESIAN_POINT('Ctrl Pts',(-2.35921176770024,0.848280000432971,
10.7914671398409));
#29989=CARTESIAN_POINT('Ctrl Pts',(-2.37545779881228,0.0353556381482985,
10.8462510684848));
#29990=CARTESIAN_POINT('Ctrl Pts',(-2.37533330856671,0.000645282184899929,
10.848589891905));
#29991=CARTESIAN_POINT('Origin',(0.,0.,-1.84858989190501));
#29992=CARTESIAN_POINT('',(-2.37515405515002,0.000755925037124906,8.65141010809499));
#29993=CARTESIAN_POINT('',(-2.36963954810708,0.00174754145538428,8.84858989190503));
#29994=CARTESIAN_POINT('',(-2.37175,-1.78696459712734E-13,-1.84858989190501));
#29995=CARTESIAN_POINT('Ctrl Pts',(-2.37515405515002,0.00075592503712492,
8.65141010809499));
#29996=CARTESIAN_POINT('Ctrl Pts',(-2.37204958700235,-0.733179040239741,
8.70085899098224));
#29997=CARTESIAN_POINT('Ctrl Pts',(-1.61660279875904,-2.25007474146859,
8.80268737837401));
#29998=CARTESIAN_POINT('Ctrl Pts',(0.954326572136137,-2.62560372673677,
8.95689527027026));
#29999=CARTESIAN_POINT('Ctrl Pts',(2.71697669134881,-0.650055649344734,
9.11403378378378));
#30000=CARTESIAN_POINT('Ctrl Pts',(2.03934512373477,1.90934627218937,9.2711722972973));
#30001=CARTESIAN_POINT('Ctrl Pts',(-0.469944521571767,2.75384968723896,
9.42831081081079));
#30002=CARTESIAN_POINT('Ctrl Pts',(-2.15345863304216,1.44000181080629,9.55505674774338));
#30003=CARTESIAN_POINT('Ctrl Pts',(-2.36963965360463,0.329676840769313,
9.62942318017144));
#30004=CARTESIAN_POINT('Ctrl Pts',(-2.36842744616303,0.000951336475575049,
9.65141010809499));
#30005=CARTESIAN_POINT('Ctrl Pts',(-2.36963954810708,0.00174754145538407,
8.84858989190503));
#30006=CARTESIAN_POINT('Ctrl Pts',(-2.36598349144566,-0.520661037292834,
8.88357647246699));
#30007=CARTESIAN_POINT('Ctrl Pts',(-1.9397431197991,-1.83158688452099,8.97100815825266));
#30008=CARTESIAN_POINT('Ctrl Pts',(0.215690902196592,-2.78647992051942,
9.11088494926201));
#30009=CARTESIAN_POINT('Ctrl Pts',(2.4459813653409,-1.35209655994371,9.26822026493315));
#30010=CARTESIAN_POINT('Ctrl Pts',(2.47433880171217,1.29947749716991,9.42555558060427));
#30011=CARTESIAN_POINT('Ctrl Pts',(0.275231669725872,2.78123058171878,9.58289089627539));
#30012=CARTESIAN_POINT('Ctrl Pts',(-1.91777323438188,1.86527979947427,9.72390233337565));
#30013=CARTESIAN_POINT('Ctrl Pts',(-2.36594419049973,0.537237102851684,
9.81246866525219));
#30014=CARTESIAN_POINT('Ctrl Pts',(-2.37005148067835,-0.0018770397834093,
9.84858989190503));
#30015=CARTESIAN_POINT('Origin',(0.,0.,-1.84858989190501));
#30016=CARTESIAN_POINT('',(-2.37012643568897,-0.00188307441280249,7.65141010809499));
#30017=CARTESIAN_POINT('',(-2.37543174471759,-0.000319652972777529,7.84858989190503));
#30018=CARTESIAN_POINT('',(-2.37175,-1.78696459712734E-13,-1.84858989190501));
#30019=CARTESIAN_POINT('Ctrl Pts',(-2.37012643568897,-0.00188307441280247,
7.65141010809499));
#30020=CARTESIAN_POINT('Ctrl Pts',(-2.37197329244753,-0.242542001652036,
7.66753579278404));
#30021=CARTESIAN_POINT('Ctrl Pts',(-2.22842022339473,-1.26275955622086,
7.7360409819776));
#30022=CARTESIAN_POINT('Ctrl Pts',(-0.770711640749916,-2.68524440462409,
7.85692567567567));
#30023=CARTESIAN_POINT('Ctrl Pts',(1.81639251383808,-2.12255793467458,8.01406418918919));
#30024=CARTESIAN_POINT('Ctrl Pts',(2.77208469636934,0.346526200869026,8.1712027027027));
#30025=CARTESIAN_POINT('Ctrl Pts',(1.23799993580832,2.50437418705365,8.32834121621622));
#30026=CARTESIAN_POINT('Ctrl Pts',(-1.40800742257503,2.4128922603655,8.48547972972973));
#30027=CARTESIAN_POINT('Ctrl Pts',(-2.35469744140074,0.865004378788607,
8.59316936035599));
#30028=CARTESIAN_POINT('Ctrl Pts',(-2.37533804356255,0.0442530790537146,
8.64847948647774));
#30029=CARTESIAN_POINT('Ctrl Pts',(-2.37515405515002,0.00075592503712492,
8.65141010809499));
#30030=CARTESIAN_POINT('Ctrl Pts',(-2.37543174471759,-0.000319652972777509,
7.84858989190503));
#30031=CARTESIAN_POINT('Ctrl Pts',(-2.37546608504675,-0.0181868229420618,
7.84979406923436));
#30032=CARTESIAN_POINT('Ctrl Pts',(-2.36724692977477,-0.814184073087101,
7.9034433517874));
#30033=CARTESIAN_POINT('Ctrl Pts',(-1.48345697628832,-2.36861723168749,
8.00953773956416));
#30034=CARTESIAN_POINT('Ctrl Pts',(1.16262680634646,-2.54151354917186,8.16687305523529));
#30035=CARTESIAN_POINT('Ctrl Pts',(2.76208455499713,-0.426475157784177,
8.3242083709064));
#30036=CARTESIAN_POINT('Ctrl Pts',(1.8750440359881,2.07248692819523,8.48154368657753));
#30037=CARTESIAN_POINT('Ctrl Pts',(-0.699958537943023,2.7057439570526,8.63887900224866));
#30038=CARTESIAN_POINT('Ctrl Pts',(-2.21235813584821,1.30404785948979,8.76122773735781));
#30039=CARTESIAN_POINT('Ctrl Pts',(-2.37146394347132,0.262432721575661,
8.83113136724327));
#30040=CARTESIAN_POINT('Ctrl Pts',(-2.36963954810708,0.00174754145538407,
8.84858989190503));
#30041=CARTESIAN_POINT('Origin',(0.,0.,-1.84858989190501));
#30042=CARTESIAN_POINT('',(-2.36973441944585,0.0017659640348839,6.65141010809499));
#30043=CARTESIAN_POINT('',(-2.36889628024144,-0.00137619754296547,6.84858989190503));
#30044=CARTESIAN_POINT('',(-2.37175,-1.78696459712734E-13,-1.84858989190501));
#30045=CARTESIAN_POINT('Ctrl Pts',(-2.36973441944585,0.00176596403488379,
6.65141010809499));
#30046=CARTESIAN_POINT('Ctrl Pts',(-2.36600087280351,-0.523508321396127,
6.68659209909035));
#30047=CARTESIAN_POINT('Ctrl Pts',(-1.93625564677593,-1.83636884117464,
6.77415359459022));
#30048=CARTESIAN_POINT('Ctrl Pts',(0.222416181733502,-2.78479173243988,
6.91409459459459));
#30049=CARTESIAN_POINT('Ctrl Pts',(2.4466042959518,-1.34857753576241,7.0712331081081));
#30050=CARTESIAN_POINT('Ctrl Pts',(2.47334911304448,1.29887571249989,7.22837162162162));
#30051=CARTESIAN_POINT('Ctrl Pts',(0.278629494786153,2.77973012269657,7.38551013513513));
#30052=CARTESIAN_POINT('Ctrl Pts',(-1.91543890246215,1.86818192765693,7.52652296395959));
#30053=CARTESIAN_POINT('Ctrl Pts',(-2.36597432596829,0.539167154048567,
7.61515628827954));
#30054=CARTESIAN_POINT('Ctrl Pts',(-2.37012643568897,-0.00188307441280247,
7.65141010809499));
#30055=CARTESIAN_POINT('Ctrl Pts',(-2.36889628024144,-0.0013761975429653,
6.84858989190503));
#30056=CARTESIAN_POINT('Ctrl Pts',(-2.37049735026751,-0.298256860301772,
6.86845677122545));
#30057=CARTESIAN_POINT('Ctrl Pts',(-2.18189218700624,-1.37689100842058,
6.94076875576958));
#30058=CARTESIAN_POINT('Ctrl Pts',(-0.57644849505612,-2.73472106868152,
7.06552584553741));
#30059=CARTESIAN_POINT('Ctrl Pts',(1.96716344393165,-1.98526073259378,7.22286116120855));
#30060=CARTESIAN_POINT('Ctrl Pts',(2.73988515609665,0.551381466653972,7.38019647687966));
#30061=CARTESIAN_POINT('Ctrl Pts',(1.04609303646807,2.5916561403346,7.53753179255079));
#30062=CARTESIAN_POINT('Ctrl Pts',(-1.56924738212969,2.3010974504224,7.69366293089257));
#30063=CARTESIAN_POINT('Ctrl Pts',(-2.3739704729535,0.759975650525201,7.79734896401065));
#30064=CARTESIAN_POINT('Ctrl Pts',(-2.37543174471759,-0.000319652972777509,
7.84858989190503));
#30065=CARTESIAN_POINT('Origin',(0.,0.,-1.84858989190501));
#30066=CARTESIAN_POINT('',(-2.37533640146812,-0.000487534612837604,5.65141010809499));
#30067=CARTESIAN_POINT('',(-2.3710171167516,0.00204493508413422,5.84858989190502));
#30068=CARTESIAN_POINT('',(-2.37175,-1.78696459712734E-13,-1.84858989190501));
#30069=CARTESIAN_POINT('Ctrl Pts',(-2.37533640146812,-0.000487534612837498,
5.65141010809499));
#30070=CARTESIAN_POINT('Ctrl Pts',(-2.3754150982357,-0.0280706202968775,
5.65326890089215));
#30071=CARTESIAN_POINT('Ctrl Pts',(-2.36258260410634,-0.832851216236821,
5.70750719819383));
#30072=CARTESIAN_POINT('Ctrl Pts',(-1.45646562934828,-2.38395507960311,
5.81412499999999));
#30073=CARTESIAN_POINT('Ctrl Pts',(1.18715361157964,-2.5288733170224,5.97126351351352));
#30074=CARTESIAN_POINT('Ctrl Pts',(2.76451839080433,-0.402457473451116,
6.12840202702702));
#30075=CARTESIAN_POINT('Ctrl Pts',(1.8589019956498,2.08542976904401,6.28554054054054));
#30076=CARTESIAN_POINT('Ctrl Pts',(-0.716306714602523,2.70026640197657,
6.44267905405405));
#30077=CARTESIAN_POINT('Ctrl Pts',(-2.21563200675447,1.29517183256302,6.5646355765722));
#30078=CARTESIAN_POINT('Ctrl Pts',(-2.37155943608083,0.258528340584143,
6.63421259458585));
#30079=CARTESIAN_POINT('Ctrl Pts',(-2.36973441944585,0.00176596403488379,
6.65141010809499));
#30080=CARTESIAN_POINT('Ctrl Pts',(-2.3710171167516,0.00204493508413416,
5.84858989190502));
#30081=CARTESIAN_POINT('Ctrl Pts',(-2.36609071130836,-0.572418580286349,
5.88711947321653));
#30082=CARTESIAN_POINT('Ctrl Pts',(-1.86927748327345,-1.93646185988882,
5.97809415975175));
#30083=CARTESIAN_POINT('Ctrl Pts',(0.401163844498212,-2.76587414046649,
6.12151395151068));
#30084=CARTESIAN_POINT('Ctrl Pts',(2.53076037597685,-1.18585163930103,6.2788492671818));
#30085=CARTESIAN_POINT('Ctrl Pts',(2.38210248511723,1.46170446446183,6.43618458285292));
#30086=CARTESIAN_POINT('Ctrl Pts',(0.0890157606711408,2.793397283841,6.59351989852405));
#30087=CARTESIAN_POINT('Ctrl Pts',(-1.98453634187054,1.75978107224967,6.73098833487474));
#30088=CARTESIAN_POINT('Ctrl Pts',(-2.36627080393209,0.485456441931073,
6.81601166600174));
#30089=CARTESIAN_POINT('Ctrl Pts',(-2.36889628024144,-0.0013761975429653,
6.84858989190503));
#30090=CARTESIAN_POINT('Origin',(0.,0.,-1.84858989190501));
#30091=CARTESIAN_POINT('',(-2.36864740940268,-0.0011676470311218,4.65141010809498));
#30092=CARTESIAN_POINT('',(-2.37471653528189,-0.00117837014130401,4.84858989190502));
#30093=CARTESIAN_POINT('',(-2.37175,-1.78696459712734E-13,-1.84858989190501));
#30094=CARTESIAN_POINT('Ctrl Pts',(-2.36864740940268,-0.00116764703112199,
4.65141010809498));
#30095=CARTESIAN_POINT('Ctrl Pts',(-2.37007090104248,-0.313795660845675,
4.67232520719846));
#30096=CARTESIAN_POINT('Ctrl Pts',(-2.16810014725707,-1.40760004764448,
4.74561981080643));
#30097=CARTESIAN_POINT('Ctrl Pts',(-0.525482821607704,-2.74379331497496,
4.87129391891892));
#30098=CARTESIAN_POINT('Ctrl Pts',(2.00035639160479,-1.95015595724574,5.02843243243243));
#30099=CARTESIAN_POINT('Ctrl Pts',(2.72955454106374,0.595034417816705,5.18557094594594));
#30100=CARTESIAN_POINT('Ctrl Pts',(1.0071746643292,2.60578839251754,5.34270945945947));
#30101=CARTESIAN_POINT('Ctrl Pts',(-1.58873507575841,2.28002578161798,5.49798918017579));
#30102=CARTESIAN_POINT('Ctrl Pts',(-2.37319747737008,0.7492017916888,5.60088939638765));
#30103=CARTESIAN_POINT('Ctrl Pts',(-2.37533640146812,-0.000487534612837498,
5.65141010809499));
#30104=CARTESIAN_POINT('Ctrl Pts',(-2.37471653528189,-0.00117837014130423,
4.84858989190502));
#30105=CARTESIAN_POINT('Ctrl Pts',(-2.37515017179056,-0.0716719020310164,
4.85333706998391));
#30106=CARTESIAN_POINT('Ctrl Pts',(-2.34054813360425,-0.920521113001663,
4.91052935328651));
#30107=CARTESIAN_POINT('Ctrl Pts',(-1.32208186928512,-2.46233460804071,
5.02016674181281));
#30108=CARTESIAN_POINT('Ctrl Pts',(1.32964132424929,-2.45826079574207,5.17750205748394));
#30109=CARTESIAN_POINT('Ctrl Pts',(2.78438780839412,-0.241198514719961,
5.33483737315506));
#30110=CARTESIAN_POINT('Ctrl Pts',(1.73255804842731,2.19299676239354,5.49217268882618));
#30111=CARTESIAN_POINT('Ctrl Pts',(-0.878964234485193,2.65300095467984,
5.64950800449731));
#30112=CARTESIAN_POINT('Ctrl Pts',(-2.25346115704322,1.19692341827648,5.76831373885692));
#30113=CARTESIAN_POINT('Ctrl Pts',(-2.37279636039799,0.20952086689332,5.83467436799283));
#30114=CARTESIAN_POINT('Ctrl Pts',(-2.3710171167516,0.00204493508413416,
5.84858989190502));
#30115=CARTESIAN_POINT('Origin',(0.,0.,-1.84858989190501));
#30116=CARTESIAN_POINT('',(-2.37165914320747,0.00205379600805495,3.65141010809498));
#30117=CARTESIAN_POINT('',(-2.36819322153198,-0.000653453332863235,3.84858989190502));
#30118=CARTESIAN_POINT('',(-2.37175,-1.78696459712734E-13,-1.84858989190501));
#30119=CARTESIAN_POINT('Ctrl Pts',(-2.37165914320747,0.0020537960080548,
3.65141010809498));
#30120=CARTESIAN_POINT('Ctrl Pts',(-2.36638740749304,-0.593495286532831,
3.69138151350476));
#30121=CARTESIAN_POINT('Ctrl Pts',(-1.83931642681201,-1.97778866762885,
3.78373242341905));
#30122=CARTESIAN_POINT('Ctrl Pts',(0.47257542983782,-2.75339906613161,3.92846283783783));
#30123=CARTESIAN_POINT('Ctrl Pts',(2.55822296043148,-1.12251023841371,4.08560135135135));
#30124=CARTESIAN_POINT('Ctrl Pts',(2.34617571991457,1.51657292659299,4.24273986486486));
#30125=CARTESIAN_POINT('Ctrl Pts',(0.0268861606557786,2.79353021925399,
4.39987837837838));
#30126=CARTESIAN_POINT('Ctrl Pts',(-2.00464048744226,1.72543877128143,4.53610179278842));
#30127=CARTESIAN_POINT('Ctrl Pts',(-2.36650592693501,0.469145905762286,
4.61994570269395));
#30128=CARTESIAN_POINT('Ctrl Pts',(-2.36864740940268,-0.00116764703112199,
4.65141010809498));
#30129=CARTESIAN_POINT('Ctrl Pts',(-2.36819322153198,-0.000653453332863235,
3.84858989190502));
#30130=CARTESIAN_POINT('Ctrl Pts',(-2.36907284142701,-0.350739660290616,
3.871999771975));
#30131=CARTESIAN_POINT('Ctrl Pts',(-2.13320735842129,-1.48399610964751,
3.94785475726868));
#30132=CARTESIAN_POINT('Ctrl Pts',(-0.392663608746353,-2.76709368867159,
4.07615484778607));
#30133=CARTESIAN_POINT('Ctrl Pts',(2.09526330020315,-1.8495577562663,4.23349016345719));
#30134=CARTESIAN_POINT('Ctrl Pts',(2.69698125586998,0.732996791565816,4.39082547912832));
#30135=CARTESIAN_POINT('Ctrl Pts',(0.870808554093777,2.65568911080063,4.54816079479944));
#30136=CARTESIAN_POINT('Ctrl Pts',(-1.66053522846232,2.20178445767042,4.70074893239168));
#30137=CARTESIAN_POINT('Ctrl Pts',(-2.37035951259304,0.707115123883991,
4.8008919647602));
#30138=CARTESIAN_POINT('Ctrl Pts',(-2.37471653528189,-0.00117837014130423,
4.84858989190502));
#30139=CARTESIAN_POINT('Origin',(0.,0.,-1.84858989190501));
#30140=CARTESIAN_POINT('',(-2.37406517885066,-0.00153607482357252,2.65141010809498));
#30141=CARTESIAN_POINT('',(-2.37255724078598,0.00199178475905649,2.84858989190502));
#30142=CARTESIAN_POINT('',(-2.37175,-1.78696459712734E-13,-1.84858989190501));
#30143=CARTESIAN_POINT('Ctrl Pts',(-2.37406517885066,-0.00153607482357281,
2.65141010809498));
#30144=CARTESIAN_POINT('Ctrl Pts',(-2.37481281249436,-0.100330398866114,
2.65805831530656));
#30145=CARTESIAN_POINT('Ctrl Pts',(-2.32469515905834,-0.976735840432517,
2.71708602702265));
#30146=CARTESIAN_POINT('Ctrl Pts',(-1.23560715428754,-2.50555554774625,
2.82849324324324));
#30147=CARTESIAN_POINT('Ctrl Pts',(1.41031161531747,-2.41154623133624,2.98563175675675));
#30148=CARTESIAN_POINT('Ctrl Pts',(2.78954424185296,-0.151581281506301,
3.14277027027027));
#30149=CARTESIAN_POINT('Ctrl Pts',(1.66331845351111,2.24452793077997,3.29990878378378));
#30150=CARTESIAN_POINT('Ctrl Pts',(-0.956834235921451,2.62469088021855,
3.45704729729729));
#30151=CARTESIAN_POINT('Ctrl Pts',(-2.26971028444252,1.15040938517441,3.57421440540103));
#30152=CARTESIAN_POINT('Ctrl Pts',(-2.37329561854466,0.186926755969883,
3.63900200900026));
#30153=CARTESIAN_POINT('Ctrl Pts',(-2.37165914320747,0.0020537960080548,
3.65141010809498));
#30154=CARTESIAN_POINT('Ctrl Pts',(-2.37255724078598,0.00199178475905658,
2.84858989190502));
#30155=CARTESIAN_POINT('Ctrl Pts',(-2.36697397570993,-0.624252704055323,
2.89066247396608));
#30156=CARTESIAN_POINT('Ctrl Pts',(-1.79321255273579,-2.04018921676783,
2.98518016125086));
#30157=CARTESIAN_POINT('Ctrl Pts',(0.584848394656438,-2.73293698550247,
3.13214295375933));
#30158=CARTESIAN_POINT('Ctrl Pts',(2.60425579784155,-1.01431944186932,3.28947826943046));
#30159=CARTESIAN_POINT('Ctrl Pts',(2.27924634057658,1.61741407950708,3.44681358510158));
#30160=CARTESIAN_POINT('Ctrl Pts',(-0.0975982492034651,2.79311059143494,
3.6041489007727));
#30161=CARTESIAN_POINT('Ctrl Pts',(-2.04600507844241,1.65356799864077,3.73807433637385));
#30162=CARTESIAN_POINT('Ctrl Pts',(-2.36710223082098,0.433557734928271,
3.81955466675129));
#30163=CARTESIAN_POINT('Ctrl Pts',(-2.36819322153198,-0.000653453332863235,
3.84858989190502));
#30164=CARTESIAN_POINT('Origin',(0.,0.,-1.84858989190501));
#30165=CARTESIAN_POINT('',(-2.36804188512505,-0.000112073902353324,1.65141010809498));
#30166=CARTESIAN_POINT('',(-2.37344137975612,-0.00178937704920473,1.84858989190502));
#30167=CARTESIAN_POINT('',(-2.37175,-1.78696459712734E-13,-1.84858989190501));
#30168=CARTESIAN_POINT('Ctrl Pts',(-2.36804188512505,-0.000112073902353224,
1.65141010809498));
#30169=CARTESIAN_POINT('Ctrl Pts',(-2.36821023678956,-0.384577180330964,
1.67711462161287));
#30170=CARTESIAN_POINT('Ctrl Pts',(-2.09930421630608,-1.55226751145704,
1.75519863963526));
#30171=CARTESIAN_POINT('Ctrl Pts',(-0.275973625536248,-2.77999224892802,
1.88566216216216));
#30172=CARTESIAN_POINT('Ctrl Pts',(2.16802781286073,-1.76187209738162,2.04280067567567));
#30173=CARTESIAN_POINT('Ctrl Pts',(2.66479327803676,0.838697048159531,2.19993918918919));
#30174=CARTESIAN_POINT('Ctrl Pts',(0.76814623510466,2.68597898024514,2.3570777027027));
#30175=CARTESIAN_POINT('Ctrl Pts',(-1.70898688612053,2.14473275169325,2.50756800900463));
#30176=CARTESIAN_POINT('Ctrl Pts',(-2.36892240045369,0.678044518839718,
2.60567881080206));
#30177=CARTESIAN_POINT('Ctrl Pts',(-2.37406517885066,-0.00153607482357281,
2.65141010809498));
#30178=CARTESIAN_POINT('Ctrl Pts',(-2.37344137975612,-0.00178937704920463,
1.84858989190502));
#30179=CARTESIAN_POINT('Ctrl Pts',(-2.37447812169567,-0.12506848067989,
1.85688007073346));
#30180=CARTESIAN_POINT('Ctrl Pts',(-2.31006431944847,-1.02714724785255,
1.91761535478561));
#30181=CARTESIAN_POINT('Ctrl Pts',(-1.15481219883121,-2.54507342378116,
2.03079574406147));
#30182=CARTESIAN_POINT('Ctrl Pts',(1.49072764255621,-2.36404822464922,2.18813105973259));
#30183=CARTESIAN_POINT('Ctrl Pts',(2.79427705549031,-0.0548463935276453,
2.34546637540372));
#30184=CARTESIAN_POINT('Ctrl Pts',(1.5823475414007,2.30372918060613,2.50280169107483));
#30185=CARTESIAN_POINT('Ctrl Pts',(-1.05405113312049,2.58842974112365,2.66013700674597));
#30186=CARTESIAN_POINT('Ctrl Pts',(-2.29031280961247,1.08993341565411,2.77539974035602));
#30187=CARTESIAN_POINT('Ctrl Pts',(-2.37393373216083,0.15638533864836,2.83821736874238));
#30188=CARTESIAN_POINT('Ctrl Pts',(-2.37255724078598,0.00199178475905658,
2.84858989190502));
#30189=CARTESIAN_POINT('Origin',(0.,0.,-1.84858989190501));
#30190=CARTESIAN_POINT('',(-2.37366757034868,0.00184471646948807,0.651410108094983));
#30191=CARTESIAN_POINT('',(-2.36802324146013,0.000186122305323028,0.848589891905023));
#30192=CARTESIAN_POINT('',(-2.37175,-1.78696459712734E-13,-1.84858989190501));
#30193=CARTESIAN_POINT('Ctrl Pts',(-2.37366757034868,0.001844716469488,
0.651410108094984));
#30194=CARTESIAN_POINT('Ctrl Pts',(-2.36827887140227,-0.663567421798888,
0.696170927919177));
#30195=CARTESIAN_POINT('Ctrl Pts',(-1.73206830317985,-2.11713322740477,
0.793311252247876));
#30196=CARTESIAN_POINT('Ctrl Pts',(0.718910407331439,-2.69944634094777,
0.942831081081078));
#30197=CARTESIAN_POINT('Ctrl Pts',(2.64899289676255,-0.887370898887054,
1.09996959459459));
#30198=CARTESIAN_POINT('Ctrl Pts',(2.19990031581894,1.72195501972256,1.25710810810811));
#30199=CARTESIAN_POINT('Ctrl Pts',(-0.225079684819506,2.78455874530281,
1.41424662162162));
#30200=CARTESIAN_POINT('Ctrl Pts',(-2.08428517335687,1.58152664346482,1.54568062161725));
#30201=CARTESIAN_POINT('Ctrl Pts',(-2.36786717732013,0.39886856587965,1.62473511710837));
#30202=CARTESIAN_POINT('Ctrl Pts',(-2.36804188512505,-0.000112073902353224,
1.65141010809498));
#30203=CARTESIAN_POINT('Ctrl Pts',(-2.36802324146013,0.000186122305323062,
0.848589891905023));
#30204=CARTESIAN_POINT('Ctrl Pts',(-2.36776001721126,-0.402962357372647,
0.87554277272455));
#30205=CARTESIAN_POINT('Ctrl Pts',(-2.0797505690667,-1.59092671500009,0.954940758767785));
#30206=CARTESIAN_POINT('Ctrl Pts',(-0.207121339063888,-2.78711087979173,
1.08678385003473));
#30207=CARTESIAN_POINT('Ctrl Pts',(2.21401803077907,-1.70561830406782,1.24411916570585));
#30208=CARTESIAN_POINT('Ctrl Pts',(2.64205485235054,0.911349150745493,1.40145448137697));
#30209=CARTESIAN_POINT('Ctrl Pts',(0.691640660298454,2.70787919402874,1.5587897970481));
#30210=CARTESIAN_POINT('Ctrl Pts',(-1.74582592441822,2.10050088985172,1.70783493389078));
#30211=CARTESIAN_POINT('Ctrl Pts',(-2.36791951286044,0.654816452515466,
1.80443496550976));
#30212=CARTESIAN_POINT('Ctrl Pts',(-2.37344137975612,-0.00178937704920463,
1.84858989190502));
#30213=CARTESIAN_POINT('Origin',(0.,0.,11.5));
#30214=CARTESIAN_POINT('',(-2.86997293948595,0.000709208322249463,11.1339652973708));
#30215=CARTESIAN_POINT('Ctrl Pts',(-0.439445221994061,2.3306835819919,11.62825));
#30216=CARTESIAN_POINT('Ctrl Pts',(-0.359483020814685,2.34931149018937,
11.6247602761445));
#30217=CARTESIAN_POINT('Ctrl Pts',(-0.27871400731898,2.36341693162049,11.6212847858384));
#30218=CARTESIAN_POINT('Ctrl Pts',(-0.197463562604575,2.37318447045242,
11.6178187998135));
#30219=CARTESIAN_POINT('Ctrl Pts',(-0.114065564321399,2.38321017787593,
11.614261203328));
#30220=CARTESIAN_POINT('Ctrl Pts',(-0.0301595928545948,2.38866567182183,
11.6107136201843));
#30221=CARTESIAN_POINT('Ctrl Pts',(0.0539178478306465,2.38969830818771,
11.6071709361129));
#30222=CARTESIAN_POINT('Ctrl Pts',(0.0934462943689916,2.39018379527021,
11.6055053668855));
#30223=CARTESIAN_POINT('Ctrl Pts',(0.133012786809523,2.38969093626847,11.6038408805234));
#30224=CARTESIAN_POINT('Ctrl Pts',(0.172582728329755,2.38823118545469,11.6021769455617));
#30225=CARTESIAN_POINT('Ctrl Pts',(0.196983674678661,2.38733102488025,11.6011508741002));
#30226=CARTESIAN_POINT('Ctrl Pts',(0.221385934120707,2.38606314465001,11.6001250123152));
#30227=CARTESIAN_POINT('Ctrl Pts',(0.24578137026875,2.38442977721171,11.5990992355836));
#30228=CARTESIAN_POINT('Ctrl Pts',(0.261730484740349,2.38336192320454,11.5984286088969));
#30229=CARTESIAN_POINT('Ctrl Pts',(0.277677591321838,2.38213767553654,11.597757980196));
#30230=CARTESIAN_POINT('Ctrl Pts',(0.293603734342933,2.38075929535175,11.5970880163414));
#30231=CARTESIAN_POINT('Ctrl Pts',(0.379341030417818,2.37333888038685,11.5934813119885));
#30232=CARTESIAN_POINT('Ctrl Pts',(0.464583014225527,2.36144918428767,11.5898891320915));
#30233=CARTESIAN_POINT('Ctrl Pts',(0.548977057540434,2.34525221307984,11.5863062427765));
#30234=CARTESIAN_POINT('Ctrl Pts',(0.63410785152571,2.32891384410355,11.5826920752337));
#30235=CARTESIAN_POINT('Ctrl Pts',(0.718376786391574,2.30819252148602,11.5790873611926));
#30236=CARTESIAN_POINT('Ctrl Pts',(0.801421129360431,2.28320149524268,11.5754867285058));
#30237=CARTESIAN_POINT('Ctrl Pts',(0.851520069054253,2.26812492443856,11.5733145410529));
#30238=CARTESIAN_POINT('Ctrl Pts',(0.901173245121242,2.25149340059607,11.5711438389925));
#30239=CARTESIAN_POINT('Ctrl Pts',(0.950298631716725,2.23332291784394,11.5689734428101));
#30240=CARTESIAN_POINT('Ctrl Pts',(0.963508179039198,2.22843697457875,11.5683898351671));
#30241=CARTESIAN_POINT('Ctrl Pts',(0.976678902975083,2.22343988211883,11.5678062771152));
#30242=CARTESIAN_POINT('Ctrl Pts',(0.989796896482515,2.2183369213822,11.5672232951128));
#30243=CARTESIAN_POINT('Ctrl Pts',(1.0715488401239,2.18653503351653,11.5635901242489));
#30244=CARTESIAN_POINT('Ctrl Pts',(1.15137916677557,2.15057972741051,11.5599737688071));
#30245=CARTESIAN_POINT('Ctrl Pts',(1.22892868995964,2.11061806082819,11.5563689172299));
#30246=CARTESIAN_POINT('Ctrl Pts',(1.30609743699769,2.07085261014462,11.5527817658451));
#30247=CARTESIAN_POINT('Ctrl Pts',(1.38100867140758,2.02711976610499,11.5492060056319));
#30248=CARTESIAN_POINT('Ctrl Pts',(1.45329568150197,1.97951483102432,11.5456364028898));
#30249=CARTESIAN_POINT('Ctrl Pts',(1.51120974849783,1.94137526215855,11.5427765500327));
#30250=CARTESIAN_POINT('Ctrl Pts',(1.56743935204678,1.90074932215926,11.5399206494764));
#30251=CARTESIAN_POINT('Ctrl Pts',(1.621783737959,1.85766460010194,11.5370660098083));
#30252=CARTESIAN_POINT('Ctrl Pts',(1.64895593091511,1.83612223907328,11.5356386899743));
#30253=CARTESIAN_POINT('Ctrl Pts',(1.67565661487015,1.81396489287275,11.5342116853624));
#30254=CARTESIAN_POINT('Ctrl Pts',(1.70185926132131,1.79119431574093,11.532784659546));
#30255=CARTESIAN_POINT('Ctrl Pts',(1.71882166156475,1.77645368090452,11.5318608680083));
#30256=CARTESIAN_POINT('Ctrl Pts',(1.73557532962421,1.76145603809249,11.5309370675846));
#30257=CARTESIAN_POINT('Ctrl Pts',(1.75211281381839,1.74620161928424,11.5300131670071));
#30258=CARTESIAN_POINT('Ctrl Pts',(1.76112158754248,1.73789179381609,11.529509873329));
#30259=CARTESIAN_POINT('Ctrl Pts',(1.77006808708219,1.72950393138366,11.5290064421071));
#30260=CARTESIAN_POINT('Ctrl Pts',(1.77894146971999,1.72104732904951,11.5285034067769));
#30261=CARTESIAN_POINT('Ctrl Pts',(1.83933200754334,1.66349331791721,11.5250798449438));
#30262=CARTESIAN_POINT('Ctrl Pts',(1.8963984276916,1.60270624192685,11.5216713230637));
#30263=CARTESIAN_POINT('Ctrl Pts',(1.95011819953022,1.53907807970147,11.5182734051049));
#30264=CARTESIAN_POINT('Ctrl Pts',(2.00542449571231,1.47357076525995,11.5147751352761));
#30265=CARTESIAN_POINT('Ctrl Pts',(2.05718398574646,1.40505149787053,11.511288104956));
#30266=CARTESIAN_POINT('Ctrl Pts',(2.10533946111886,1.3339039115796,11.5078074733588));
#30267=CARTESIAN_POINT('Ctrl Pts',(2.15154257592138,1.26564085173229,11.5044679565119));
#30268=CARTESIAN_POINT('Ctrl Pts',(2.19442802485129,1.19495736996561,11.5011343300606));
#30269=CARTESIAN_POINT('Ctrl Pts',(2.23391281993103,1.12216394079048,11.4978023184486));
#30270=CARTESIAN_POINT('Ctrl Pts',(2.25118741777841,1.09031681552637,11.4963445633684));
#30271=CARTESIAN_POINT('Ctrl Pts',(2.26781067606573,1.05806553560368,11.4948871173785));
#30272=CARTESIAN_POINT('Ctrl Pts',(2.28377353610697,1.02543493097626,11.4934296224428));
#30273=CARTESIAN_POINT('Ctrl Pts',(2.29326703470383,1.00602872191068,11.4925628149854));
#30274=CARTESIAN_POINT('Ctrl Pts',(2.30252692730832,0.986488335264957,11.4916959902159));
#30275=CARTESIAN_POINT('Ctrl Pts',(2.31155107931692,0.966818908506685,11.4908290728209));
#30276=CARTESIAN_POINT('Ctrl Pts',(2.31863529945096,0.951377840034761,11.490148517611));
#30277=CARTESIAN_POINT('Ctrl Pts',(2.32557538886546,0.935854346809815,11.4894677807698));
#30278=CARTESIAN_POINT('Ctrl Pts',(2.33236053374086,0.920273937348818,11.4887878255595));
#30279=CARTESIAN_POINT('Ctrl Pts',(2.36796902716184,0.838507826532316,11.4852194152932));
#30280=CARTESIAN_POINT('Ctrl Pts',(2.39937221583678,0.755052917299449,11.4816670269197));
#30281=CARTESIAN_POINT('Ctrl Pts',(2.42650990964853,0.670313949715511,11.4781256336386));
#30282=CARTESIAN_POINT('Ctrl Pts',(2.45395171326163,0.584625382258507,11.4745445548773));
#30283=CARTESIAN_POINT('Ctrl Pts',(2.47703230477293,0.497622920338958,11.470974719015));
#30284=CARTESIAN_POINT('Ctrl Pts',(2.49564463758615,0.409696684762178,11.4674109283565));
#30285=CARTESIAN_POINT('Ctrl Pts',(2.51256694354607,0.329754279086013,11.464170735066));
#30286=CARTESIAN_POINT('Ctrl Pts',(2.52579526118549,0.24904737731457,11.460935538995));
#30287=CARTESIAN_POINT('Ctrl Pts',(2.53521313973642,0.167858755145902,11.4577014336506));
#30288=CARTESIAN_POINT('Ctrl Pts',(2.53942638325848,0.131537684050459,11.4562546032081));
#30289=CARTESIAN_POINT('Ctrl Pts',(2.54287653840534,0.0951201284473648,
11.4548079910601));
#30290=CARTESIAN_POINT('Ctrl Pts',(2.54555076253572,0.0586312673898904,
11.4533612474409));
#30291=CARTESIAN_POINT('Ctrl Pts',(2.54678080763582,0.0418477284777441,
11.4526957983935));
#30292=CARTESIAN_POINT('Ctrl Pts',(2.54784667039524,0.0250491043820508,
11.4520303215313));
#30293=CARTESIAN_POINT('Ctrl Pts',(2.54874698931854,0.00823785327091157,
11.4513647828174));
#30294=CARTESIAN_POINT('Ctrl Pts',(2.54950258918657,-0.00587112388394168,
11.4508062241208));
#30295=CARTESIAN_POINT('Ctrl Pts',(2.55014158604825,-0.0199907301096276,
11.4502475533557));
#30296=CARTESIAN_POINT('Ctrl Pts',(2.55066270854233,-0.0341027028361791,
11.4496894146469));
#30297=CARTESIAN_POINT('Ctrl Pts',(2.55400035119776,-0.124485909584641,
11.4461146935723));
#30298=CARTESIAN_POINT('Ctrl Pts',(2.55251590030915,-0.214700787372498,
11.4425560101414));
#30299=CARTESIAN_POINT('Ctrl Pts',(2.54610973516166,-0.304360270645855,
11.4390083150826));
#30300=CARTESIAN_POINT('Ctrl Pts',(2.53992350143221,-0.390941635131681,
11.4355824166973));
#30301=CARTESIAN_POINT('Ctrl Pts',(2.52914771427487,-0.477005973362024,
11.4321667651471));
#30302=CARTESIAN_POINT('Ctrl Pts',(2.51364702202946,-0.56221151242787,11.4287568135539));
#30303=CARTESIAN_POINT('Ctrl Pts',(2.4978416408886,-0.649091891634602,11.4252798343488));
#30304=CARTESIAN_POINT('Ctrl Pts',(2.47712400969773,-0.735080204165537,
11.4218087813851));
#30305=CARTESIAN_POINT('Ctrl Pts',(2.45176245019841,-0.819915179815436,
11.4183388343531));
#30306=CARTESIAN_POINT('Ctrl Pts',(2.43759878319083,-0.867292958210081,
11.4164009734618));
#30307=CARTESIAN_POINT('Ctrl Pts',(2.42198578511571,-0.914310849766526,
11.4144634574981));
#30308=CARTESIAN_POINT('Ctrl Pts',(2.40496360252248,-0.960921226687823,
11.4125254468584));
#30309=CARTESIAN_POINT('Ctrl Pts',(2.39839032938233,-0.978920254544038,
11.4117770661373));
#30310=CARTESIAN_POINT('Ctrl Pts',(2.39160484182306,-0.996863365779891,
11.4110284061025));
#30311=CARTESIAN_POINT('Ctrl Pts',(2.38462104532031,-1.01471861919519,11.4102806421704));
#30312=CARTESIAN_POINT('Ctrl Pts',(2.35196925304181,-1.09819843212604,11.4067845734384));
#30313=CARTESIAN_POINT('Ctrl Pts',(2.31495075727319,-1.17986515814379,11.4033036769767));
#30314=CARTESIAN_POINT('Ctrl Pts',(2.27389075093231,-1.25946542646749,11.3998332297369));
#30315=CARTESIAN_POINT('Ctrl Pts',(2.23207387867294,-1.34053297976178,11.3962988111666));
#30316=CARTESIAN_POINT('Ctrl Pts',(2.18606471254661,-1.41945796930655,11.3927752305933));
#30317=CARTESIAN_POINT('Ctrl Pts',(2.13615274225743,-1.49596025824322,11.3892574989426));
#30318=CARTESIAN_POINT('Ctrl Pts',(2.08602408315185,-1.57279467573233,11.385724495342));
#30319=CARTESIAN_POINT('Ctrl Pts',(2.03195810671375,-1.64718611516111,11.3821973915595));
#30320=CARTESIAN_POINT('Ctrl Pts',(1.97420160691916,-1.71882633760539,11.3786711332592));
#30321=CARTESIAN_POINT('Ctrl Pts',(1.95240508667088,-1.74586238661548,11.377340371168));
#30322=CARTESIAN_POINT('Ctrl Pts',(1.93008253152955,-1.77250629512415,11.3760097294909));
#30323=CARTESIAN_POINT('Ctrl Pts',(1.90724574604483,-1.79874022848494,11.3746789365696));
#30324=CARTESIAN_POINT('Ctrl Pts',(1.89585779635524,-1.81182222347379,11.3740153141501));
#30325=CARTESIAN_POINT('Ctrl Pts',(1.8843419621495,-1.82480225835256,11.3733516541209));
#30326=CARTESIAN_POINT('Ctrl Pts',(1.87269964124851,-1.83767804526001,11.3726879227956));
#30327=CARTESIAN_POINT('Ctrl Pts',(1.86326625859819,-1.8481108640987,11.3721501235353));
#30328=CARTESIAN_POINT('Ctrl Pts',(1.8537496389451,-1.8584753407347,11.3716122696922));
#30329=CARTESIAN_POINT('Ctrl Pts',(1.8441608279676,-1.86875948192732,11.3710749125616));
#30330=CARTESIAN_POINT('Ctrl Pts',(1.78056218360928,-1.93696996597738,11.3675108434478));
#30331=CARTESIAN_POINT('Ctrl Pts',(1.71368420494736,-2.00176842633816,11.3639624618779));
#30332=CARTESIAN_POINT('Ctrl Pts',(1.64382533951827,-2.06287172496906,11.3604247664903));
#30333=CARTESIAN_POINT('Ctrl Pts',(1.57423141411002,-2.12374328910052,11.3569004878264));
#30334=CARTESIAN_POINT('Ctrl Pts',(1.50167852811227,-2.18094842953722,11.3533868144436));
#30335=CARTESIAN_POINT('Ctrl Pts',(1.42641996197867,-2.2341772386581,11.3498788016679));
#30336=CARTESIAN_POINT('Ctrl Pts',(1.3516762241841,-2.28704192046701,11.3463947864845));
#30337=CARTESIAN_POINT('Ctrl Pts',(1.27426307539374,-2.33598522008376,11.342916354727));
#30338=CARTESIAN_POINT('Ctrl Pts',(1.19439676647842,-2.38066281826916,11.339438662505));
#30339=CARTESIAN_POINT('Ctrl Pts',(1.15339338620205,-2.40360030684365,11.3376532145659));
#30340=CARTESIAN_POINT('Ctrl Pts',(1.11174294293827,-2.42541271468527,11.3358679615534));
#30341=CARTESIAN_POINT('Ctrl Pts',(1.06947220915485,-2.44604826098259,11.334082247983));
#30342=CARTESIAN_POINT('Ctrl Pts',(1.05124776879456,-2.45494499044852,11.3333123623541));
#30343=CARTESIAN_POINT('Ctrl Pts',(1.0329023157667,-2.46362538871231,11.3325421557385));
#30344=CARTESIAN_POINT('Ctrl Pts',(1.01446903163988,-2.47207123914098,11.3317728670993));
#30345=CARTESIAN_POINT('Ctrl Pts',(0.992379075227472,-2.48219252119531,
11.3308509720972));
#30346=CARTESIAN_POINT('Ctrl Pts',(0.970156538466361,-2.49198036655811,
11.3299301186847));
#30347=CARTESIAN_POINT('Ctrl Pts',(0.94780620569595,-2.50142961190602,11.3290102203308));
#30348=CARTESIAN_POINT('Ctrl Pts',(0.865790439448149,-2.53610413356231,
11.3256346031023));
#30349=CARTESIAN_POINT('Ctrl Pts',(0.78205610317221,-2.56622272676918,11.3222718463403));
#30350=CARTESIAN_POINT('Ctrl Pts',(0.696974578785958,-2.59191739767486,
11.318917674299));
#30351=CARTESIAN_POINT('Ctrl Pts',(0.609579162327931,-2.61831086536073,
11.3154722816062));
#30352=CARTESIAN_POINT('Ctrl Pts',(0.520761565645775,-2.64003666842693,
11.3120359469267));
#30353=CARTESIAN_POINT('Ctrl Pts',(0.430899300361841,-2.65718927641842,
11.3086040360895));
#30354=CARTESIAN_POINT('Ctrl Pts',(0.343209845834361,-2.67392714557567,
11.3052551066101));
#30355=CARTESIAN_POINT('Ctrl Pts',(0.25452479015491,-2.6863100783274,11.3019103896282));
#30356=CARTESIAN_POINT('Ctrl Pts',(0.165183352753207,-2.69438132192965,
11.2985655790638));
#30357=CARTESIAN_POINT('Ctrl Pts',(0.137834848150192,-2.69685202812409,
11.2975416917191));
#30358=CARTESIAN_POINT('Ctrl Pts',(0.110424801620538,-2.69891839950379,
11.2965177956053));
#30359=CARTESIAN_POINT('Ctrl Pts',(0.08296290180991,-2.70058085938097,11.2954937672061));
#30360=CARTESIAN_POINT('Ctrl Pts',(0.0669684788561147,-2.70154911309258,
11.2948973502268));
#30361=CARTESIAN_POINT('Ctrl Pts',(0.0509564666454086,-2.70238034652659,
11.2943008883741));
#30362=CARTESIAN_POINT('Ctrl Pts',(0.0349287839010169,-2.70307458363613,
11.2937043572455));
#30363=CARTESIAN_POINT('Ctrl Pts',(0.0206834334719444,-2.70369161924033,
11.293174162388));
#30364=CARTESIAN_POINT('Ctrl Pts',(0.00643409067270473,-2.70420004997344,
11.2926442249703));
#30365=CARTESIAN_POINT('Ctrl Pts',(-0.00781400179505987,-2.70460019597085,
11.2921146711228));
#30366=CARTESIAN_POINT('Ctrl Pts',(-0.101952151334104,-2.70724398873305,
11.2886158715889));
#30367=CARTESIAN_POINT('Ctrl Pts',(-0.196088226677417,-2.7051673117304,
11.2851318105594));
#30368=CARTESIAN_POINT('Ctrl Pts',(-0.289825667638303,-2.6984813516168,
11.2816577549713));
#30369=CARTESIAN_POINT('Ctrl Pts',(-0.384631538117472,-2.69171918420471,
11.2781441017209));
#30370=CARTESIAN_POINT('Ctrl Pts',(-0.479030586990251,-2.68024208441543,
11.2746406832979));
#30371=CARTESIAN_POINT('Ctrl Pts',(-0.57262152425153,-2.66411259564997,
11.2711426029439));
#30372=CARTESIAN_POINT('Ctrl Pts',(-0.666559717691804,-2.64792326065578,
11.2676315434484));
#30373=CARTESIAN_POINT('Ctrl Pts',(-0.759684799865766,-2.62704692522732,
11.2641258617076));
#30374=CARTESIAN_POINT('Ctrl Pts',(-0.851585181919148,-2.6014943492988,
11.2606206062542));
#30375=CARTESIAN_POINT('Ctrl Pts',(-0.886047825189167,-2.59191213332561,
11.2593061354592));
#30376=CARTESIAN_POINT('Ctrl Pts',(-0.920338108563248,-2.58167179563189,
11.2579917246108));
#30377=CARTESIAN_POINT('Ctrl Pts',(-0.95443366677234,-2.57077201863537,
11.2566771125966));
#30378=CARTESIAN_POINT('Ctrl Pts',(-0.974280480974564,-2.5644273256531,
11.255911885049));
#30379=CARTESIAN_POINT('Ctrl Pts',(-0.99406130744013,-2.55785917358927,
11.2551465893396));
#30380=CARTESIAN_POINT('Ctrl Pts',(-1.01377165408274,-2.55106714297751,
11.2543811739687));
#30381=CARTESIAN_POINT('Ctrl Pts',(-1.02736841414217,-2.54638180627496,
11.2538531685848));
#30382=CARTESIAN_POINT('Ctrl Pts',(-1.04092225787931,-2.54159315279905,
11.253325470206));
#30383=CARTESIAN_POINT('Ctrl Pts',(-1.05443025528497,-2.53670205395909,
11.252798124302));
#30384=CARTESIAN_POINT('Ctrl Pts',(-1.14463510839177,-2.50403985843604,
11.2492765690056));
#30385=CARTESIAN_POINT('Ctrl Pts',(-1.23281912858369,-2.46680540724472,
11.2457698275395));
#30386=CARTESIAN_POINT('Ctrl Pts',(-1.31858159439492,-2.42506535814129,
11.242273074989));
#30387=CARTESIAN_POINT('Ctrl Pts',(-1.40311199337542,-2.38392494816353,
11.2388265569179));
#30388=CARTESIAN_POINT('Ctrl Pts',(-1.48529083212456,-2.33840727081253,
11.2353897428216));
#30389=CARTESIAN_POINT('Ctrl Pts',(-1.56472199239298,-2.28852750879454,
11.2319580127567));
#30390=CARTESIAN_POINT('Ctrl Pts',(-1.58551758994019,-2.27546866069046,
11.2310595633688));
#30391=CARTESIAN_POINT('Ctrl Pts',(-1.60612474663732,-2.26211056997792,
11.230161462454));
#30392=CARTESIAN_POINT('Ctrl Pts',(-1.62653609083598,-2.2484529714829,11.2292636271078));
#30393=CARTESIAN_POINT('Ctrl Pts',(-1.70441968299709,-2.19633965543995,
11.225837755629));
#30394=CARTESIAN_POINT('Ctrl Pts',(-1.77945485532057,-2.13986885585993,
11.222415750716));
#30395=CARTESIAN_POINT('Ctrl Pts',(-1.85149349468849,-2.07939019092048,
11.2189930066095));
#30396=CARTESIAN_POINT('Ctrl Pts',(-1.8748645479439,-2.05976946915896,11.2178825867641));
#30397=CARTESIAN_POINT('Ctrl Pts',(-1.89791995295043,-2.03972659946025,
11.2167720891179));
#30398=CARTESIAN_POINT('Ctrl Pts',(-1.92065386067013,-2.01927267290743,
11.2156613564032));
#30399=CARTESIAN_POINT('Ctrl Pts',(-1.9316413592642,-2.00938710936888,11.2151245294621));
#30400=CARTESIAN_POINT('Ctrl Pts',(-1.94255421950186,-1.99940498570623,
11.2145876221361));
#30401=CARTESIAN_POINT('Ctrl Pts',(-1.95338011991677,-1.98933864610605,
11.2140511999421));
#30402=CARTESIAN_POINT('Ctrl Pts',(-2.02242773931489,-1.92513550744723,
11.2106298978731));
#30403=CARTESIAN_POINT('Ctrl Pts',(-2.08805585991204,-1.85740773886018,
11.2072227031525));
#30404=CARTESIAN_POINT('Ctrl Pts',(-2.15015903930769,-1.7865606665237,11.2038251982962));
#30405=CARTESIAN_POINT('Ctrl Pts',(-2.21349481278046,-1.71430745552261,
11.2003602613952));
#30406=CARTESIAN_POINT('Ctrl Pts',(-2.27316487566809,-1.63880924004706,
11.1969054028151));
#30407=CARTESIAN_POINT('Ctrl Pts',(-2.32902567586957,-1.56045035084564,
11.1934559367882));
#30408=CARTESIAN_POINT('Ctrl Pts',(-2.38527990190259,-1.48153958249049,
11.1899821762823));
#30409=CARTESIAN_POINT('Ctrl Pts',(-2.43767154642151,-1.39972691196139,
11.1865138845562));
#30410=CARTESIAN_POINT('Ctrl Pts',(-2.48601414345046,-1.31537014370798,
11.1830462761383));
#30411=CARTESIAN_POINT('Ctrl Pts',(-2.51324863986033,-1.26784654664574,
11.1810927491288));
#30412=CARTESIAN_POINT('Ctrl Pts',(-2.53919729042327,-1.21951494628862,
11.1791394389872));
#30413=CARTESIAN_POINT('Ctrl Pts',(-2.56382026308967,-1.17043597842562,
11.1771854900701));
#30414=CARTESIAN_POINT('Ctrl Pts',(-2.57043915220293,-1.15724308533024,
11.1766602500274));
#30415=CARTESIAN_POINT('Ctrl Pts',(-2.57696321367054,-1.1439941193146,11.1761348825453));
#30416=CARTESIAN_POINT('Ctrl Pts',(-2.58338840616944,-1.13069688731366,
11.175609633533));
#30417=CARTESIAN_POINT('Ctrl Pts',(-2.62620034331217,-1.04209561027884,
11.172109827464));
#30418=CARTESIAN_POINT('Ctrl Pts',(-2.66450788394824,-0.951602474453648,
11.1686250464566));
#30419=CARTESIAN_POINT('Ctrl Pts',(-2.69817002472794,-0.859613847080416,
11.1651505728457));
#30420=CARTESIAN_POINT('Ctrl Pts',(-2.73183382450822,-0.767620686151626,
11.1616759279993));
#30421=CARTESIAN_POINT('Ctrl Pts',(-2.76085223666098,-0.67413102162785,
11.1582115915653));
#30422=CARTESIAN_POINT('Ctrl Pts',(-2.78504109696179,-0.579512179774996,
11.1547528451809));
#30423=CARTESIAN_POINT('Ctrl Pts',(-2.80867562760501,-0.487061692675289,
11.1513733619645));
#30424=CARTESIAN_POINT('Ctrl Pts',(-2.8276996967141,-0.393532337548253,
11.1479992155222));
#30425=CARTESIAN_POINT('Ctrl Pts',(-2.84189514122644,-0.299251761426908,
11.1446260045022));
#30426=CARTESIAN_POINT('Ctrl Pts',(-2.85324010443846,-0.223902964369238,
11.1419301428196));
#30427=CARTESIAN_POINT('Ctrl Pts',(-2.86150015598816,-0.148073915036915,
11.1392348786069));
#30428=CARTESIAN_POINT('Ctrl Pts',(-2.86653995619031,-0.0719300717664526,
11.1365379651471));
#30429=CARTESIAN_POINT('Ctrl Pts',(-2.86814414143213,-0.0476932320643782,
11.1356795285827));
#30430=CARTESIAN_POINT('Ctrl Pts',(-2.86941988081495,-0.0234547494955555,
11.1348219958471));
#30431=CARTESIAN_POINT('Ctrl Pts',(-2.87036479087719,0.000779773978368722,
11.1339652973708));
#30432=CARTESIAN_POINT('',(0.261199069988913,2.92594434598213,11.058));
#30433=CARTESIAN_POINT('Ctrl Pts',(0.261124777554784,2.92529416030266,11.058));
#30434=CARTESIAN_POINT('Ctrl Pts',(0.163252076286772,2.9214051496811,11.0703793245688));
#30435=CARTESIAN_POINT('Ctrl Pts',(0.0658388360676064,2.91286361031638,
11.0828028087884));
#30436=CARTESIAN_POINT('Ctrl Pts',(-0.0307369711720644,2.89968653111402,
11.0952900032599));
#30437=CARTESIAN_POINT('Ctrl Pts',(-0.12623809978967,2.88665608413482,11.1076382424244));
#30438=CARTESIAN_POINT('Ctrl Pts',(-0.220921197195477,2.86909236615812,
11.1200487818169));
#30439=CARTESIAN_POINT('Ctrl Pts',(-0.31439997383375,2.84696555496448,11.1325405266072));
#30440=CARTESIAN_POINT('Ctrl Pts',(-0.389995520831668,2.82907177783499,
11.1426425017756));
#30441=CARTESIAN_POINT('Ctrl Pts',(-0.464803253647579,2.80819289824412,
11.152797583885));
#30442=CARTESIAN_POINT('Ctrl Pts',(-0.538603048202427,2.78429272567688,
11.1630157713274));
#30443=CARTESIAN_POINT('Ctrl Pts',(-0.593952894118562,2.76636759625145,
11.1706794119091));
#30444=CARTESIAN_POINT('Ctrl Pts',(-0.648735503576454,2.7467426089957,11.1783785492407));
#30445=CARTESIAN_POINT('Ctrl Pts',(-0.702851172581185,2.72539620337798,
11.1861174013937));
#30446=CARTESIAN_POINT('Ctrl Pts',(-0.71873840261759,2.71912934457837,11.1883893667345));
#30447=CARTESIAN_POINT('Ctrl Pts',(-0.734568107078247,2.71271408483162,
11.190664755044));
#30448=CARTESIAN_POINT('Ctrl Pts',(-0.750337652372167,2.70614979460715,
11.1929436730527));
#30449=CARTESIAN_POINT('Ctrl Pts',(-0.763539656096334,2.70065427889159,
11.1948515456945));
#30450=CARTESIAN_POINT('Ctrl Pts',(-0.776691326847496,2.69505769580723,
11.1967607130315));
#30451=CARTESIAN_POINT('Ctrl Pts',(-0.789788993683481,2.68936106997679,
11.1986708957826));
#30452=CARTESIAN_POINT('Ctrl Pts',(-0.87317349082548,2.65309428397392,11.2108318119326));
#30453=CARTESIAN_POINT('Ctrl Pts',(-0.954403883416443,2.61276259333994,
11.2230385405707));
#30454=CARTESIAN_POINT('Ctrl Pts',(-1.03314628688233,2.56834468618871,11.2353100289649));
#30455=CARTESIAN_POINT('Ctrl Pts',(-1.07823214235908,2.54291214597843,11.2423363645588));
#30456=CARTESIAN_POINT('Ctrl Pts',(-1.12250179725942,2.51613922516579,11.2493839310575));
#30457=CARTESIAN_POINT('Ctrl Pts',(-1.16588734321926,2.48801620495338,11.2564562851141));
#30458=CARTESIAN_POINT('Ctrl Pts',(-1.2435976078222,2.43764349916415,11.2691239718505));
#30459=CARTESIAN_POINT('Ctrl Pts',(-1.31847408700313,2.38294042952196,11.2818711829841));
#30460=CARTESIAN_POINT('Ctrl Pts',(-1.39030087935118,2.32423346489716,11.2947183566611));
#30461=CARTESIAN_POINT('Ctrl Pts',(-1.46342993694969,2.26446210581046,11.3077984577361));
#30462=CARTESIAN_POINT('Ctrl Pts',(-1.53339828473794,2.20053932645019,11.3209821789827));
#30463=CARTESIAN_POINT('Ctrl Pts',(-1.59992558939365,2.1327921427514,11.3342910904939));
#30464=CARTESIAN_POINT('Ctrl Pts',(-1.61340208445737,2.11906853570881,11.3369870884937));
#30465=CARTESIAN_POINT('Ctrl Pts',(-1.62674073455187,2.10518403555254,11.3396889690338));
#30466=CARTESIAN_POINT('Ctrl Pts',(-1.63991787601809,2.09116421105248,11.3423925384684));
#30467=CARTESIAN_POINT('Ctrl Pts',(-1.70139884650346,2.02575150993609,11.3550066606613));
#30468=CARTESIAN_POINT('Ctrl Pts',(-1.75944768512028,1.95731714657644,11.3676731670409));
#30469=CARTESIAN_POINT('Ctrl Pts',(-1.8138993651727,1.88618389956551,11.3804137020214));
#30470=CARTESIAN_POINT('Ctrl Pts',(-1.86815753562372,1.81530344486993,11.393108959871));
#30471=CARTESIAN_POINT('Ctrl Pts',(-1.91884436205444,1.74174225535381,11.4058777210929));
#30472=CARTESIAN_POINT('Ctrl Pts',(-1.96574838356875,1.66580180077525,11.4187414001618));
#30473=CARTESIAN_POINT('Ctrl Pts',(-2.01186212788083,1.59114085290088,11.4313883414761));
#30474=CARTESIAN_POINT('Ctrl Pts',(-2.05431959945996,1.51417923664983,11.4441270290762));
#30475=CARTESIAN_POINT('Ctrl Pts',(-2.09287020326133,1.43520021222363,11.4569778131465));
#30476=CARTESIAN_POINT('Ctrl Pts',(-2.11361694660402,1.39269614256837,11.4638937079073));
#30477=CARTESIAN_POINT('Ctrl Pts',(-2.13323129045024,1.34960780406157,11.4708420687169));
#30478=CARTESIAN_POINT('Ctrl Pts',(-2.15166787184208,1.30598030868302,11.4778260675126));
#30479=CARTESIAN_POINT('Ctrl Pts',(-2.15713184571921,1.29305060712901,11.4798958865407));
#30480=CARTESIAN_POINT('Ctrl Pts',(-2.16249308944786,1.28007170317631,11.4819691313049));
#30481=CARTESIAN_POINT('Ctrl Pts',(-2.16774797314523,1.26705068510794,11.4840449452013));
#30482=CARTESIAN_POINT('Ctrl Pts',(-2.19963752356477,1.18803192158837,11.4966421358759));
#30483=CARTESIAN_POINT('Ctrl Pts',(-2.22751419897903,1.10771397257159,11.5092939385505));
#30484=CARTESIAN_POINT('Ctrl Pts',(-2.25120331746379,1.02636717479289,11.5220225137828));
#30485=CARTESIAN_POINT('Ctrl Pts',(-2.27454503464211,0.946213329121761,
11.5345644242532));
#30486=CARTESIAN_POINT('Ctrl Pts',(-2.29382118362004,0.865059764231561,
11.5471808720505));
#30487=CARTESIAN_POINT('Ctrl Pts',(-2.30881496364231,0.783166675687281,
11.5598930570057));
#30488=CARTESIAN_POINT('Ctrl Pts',(-2.3233692591387,0.703673965509062,11.572232633548));
#30489=CARTESIAN_POINT('Ctrl Pts',(-2.33388845327117,0.623483808186223,
11.5846624171728));
#30490=CARTESIAN_POINT('Ctrl Pts',(-2.34012749274977,0.542846284442329,
11.5972017976454));
#30491=CARTESIAN_POINT('Ctrl Pts',(-2.34523853245788,0.476787785015864,
11.6074740954455));
#30492=CARTESIAN_POINT('Ctrl Pts',(-2.34747636127652,0.410429125649976,
11.6178199429796));
#30493=CARTESIAN_POINT('Ctrl Pts',(-2.34668236863853,0.343918483395475,
11.62825));
#30494=CARTESIAN_POINT('',(-2.14415473270599,2.01243073062329,11.058));
#30495=CARTESIAN_POINT('Origin',(0.,0.,11.058));
#30496=CARTESIAN_POINT('Ctrl Pts',(-2.87036479087719,0.000779773978368722,
11.1339652973708));
#30497=CARTESIAN_POINT('Ctrl Pts',(-2.87200285191233,0.0427918449624727,
11.1324801566689));
#30498=CARTESIAN_POINT('Ctrl Pts',(-2.87264678506693,0.0847919926152422,
11.1309975229776));
#30499=CARTESIAN_POINT('Ctrl Pts',(-2.87228289058568,0.126751532711213,
11.1295170338848));
#30500=CARTESIAN_POINT('Ctrl Pts',(-2.87145802595519,0.221864106052536,
11.1261611075067));
#30501=CARTESIAN_POINT('Ctrl Pts',(-2.86545855469524,0.316767622116373,
11.1228162005919));
#30502=CARTESIAN_POINT('Ctrl Pts',(-2.85455763680452,0.411156736693552,
11.1194780920563));
#30503=CARTESIAN_POINT('Ctrl Pts',(-2.84342076253498,0.507588955704657,
11.1160677283208));
#30504=CARTESIAN_POINT('Ctrl Pts',(-2.82716775830471,0.603485022278454,
11.1126644604589));
#30505=CARTESIAN_POINT('Ctrl Pts',(-2.80603441756026,0.698520670355508,
11.1092637873076));
#30506=CARTESIAN_POINT('Ctrl Pts',(-2.79266006313991,0.75866451866233,11.1071116520374));
#30507=CARTESIAN_POINT('Ctrl Pts',(-2.77733000149192,0.818463754777881,
11.1049605559651));
#30508=CARTESIAN_POINT('Ctrl Pts',(-2.76009348614301,0.877834296726592,
11.1028093582138));
#30509=CARTESIAN_POINT('Ctrl Pts',(-2.74919109087412,0.915387195473845,
11.1014486882808));
#30510=CARTESIAN_POINT('Ctrl Pts',(-2.73752580613221,0.952768545576029,
11.1000879776682));
#30511=CARTESIAN_POINT('Ctrl Pts',(-2.72510854264357,0.989956497598032,
11.0987269376699));
#30512=CARTESIAN_POINT('Ctrl Pts',(-2.72027063675402,1.00444534308902,11.0981966611375));
#30513=CARTESIAN_POINT('Ctrl Pts',(-2.71531799003855,1.0189064745382,11.0976662739811));
#30514=CARTESIAN_POINT('Ctrl Pts',(-2.71025302608607,1.03333338889234,11.0971359498549));
#30515=CARTESIAN_POINT('Ctrl Pts',(-2.67741979989202,1.12685471435798,11.0936981658637));
#30516=CARTESIAN_POINT('Ctrl Pts',(-2.63998428261572,1.2186200392303,11.0902747408666));
#30517=CARTESIAN_POINT('Ctrl Pts',(-2.59822193704792,1.30830487286322,11.0868612068006));
#30518=CARTESIAN_POINT('Ctrl Pts',(-2.55598691495593,1.39900478155616,11.0834090375144));
#30519=CARTESIAN_POINT('Ctrl Pts',(-2.50932621498891,1.48757769234242,11.0799669843223));
#30520=CARTESIAN_POINT('Ctrl Pts',(-2.45847158858181,1.57367848927911,11.0765304257261));
#30521=CARTESIAN_POINT('Ctrl Pts',(-2.40788866695146,1.65931926911486,11.0731122278858));
#30522=CARTESIAN_POINT('Ctrl Pts',(-2.35315604081231,1.74251510638125,11.0696994660854));
#30523=CARTESIAN_POINT('Ctrl Pts',(-2.29445585803367,1.82290449738493,11.0662875925062));
#30524=CARTESIAN_POINT('Ctrl Pts',(-2.24693123162509,1.88798906090443,11.0635252839489));
#30525=CARTESIAN_POINT('Ctrl Pts',(-2.19680500482205,1.95123384018432,11.0607635576017));
#30526=CARTESIAN_POINT('Ctrl Pts',(-2.14415473270599,2.01243073062329,11.058));
#30527=CARTESIAN_POINT('',(-2.,-2.4492935982947E-16,12.));
#30528=CARTESIAN_POINT('',(-2.5,-3.06161699786838E-16,11.5));
#30529=CARTESIAN_POINT('Origin',(0.,0.,12.));
#30530=CARTESIAN_POINT('Ctrl Pts',(1.70810875200395,-2.39535560853238,-0.329233991005387));
#30531=CARTESIAN_POINT('Ctrl Pts',(2.49644455514999,-1.833199709811,-0.276854486500882));
#30532=CARTESIAN_POINT('Ctrl Pts',(3.46233357982621,0.120022568706166,-0.172095477491873));
#30533=CARTESIAN_POINT('Ctrl Pts',(1.80423238277522,2.96114098648209,-0.0149569639783592));
#30534=CARTESIAN_POINT('Ctrl Pts',(-1.47579564172449,3.13432118289611,0.142181549535154));
#30535=CARTESIAN_POINT('Ctrl Pts',(-3.42956675747562,0.496557026061836,
0.299320063048668));
#30536=CARTESIAN_POINT('Ctrl Pts',(-2.30343226514234,-2.58935922774548,
0.456458576562181));
#30537=CARTESIAN_POINT('Ctrl Pts',(0.891761112414455,-3.34848577424617,
0.613597090075694));
#30538=CARTESIAN_POINT('Ctrl Pts',(3.2859015926111,-1.1007252807108,0.770735603589207));
#30539=CARTESIAN_POINT('Ctrl Pts',(2.7288317609948,2.13597203247546,0.927874117102722));
#30540=CARTESIAN_POINT('Ctrl Pts',(-0.27919655644097,3.45406211813255,1.08501263061624));
#30541=CARTESIAN_POINT('Ctrl Pts',(-3.03644606033952,1.66993460430069,1.24215114412975));
#30542=CARTESIAN_POINT('Ctrl Pts',(-3.06648780987738,-1.61410638094873,
1.39928965764326));
#30543=CARTESIAN_POINT('Ctrl Pts',(-0.342327145073366,-3.44839767949667,
1.55642817115678));
#30544=CARTESIAN_POINT('Ctrl Pts',(2.68929601578421,-2.18548654390084,1.71356668467029));
#30545=CARTESIAN_POINT('Ctrl Pts',(3.30550092715682,1.04034856780235,1.8707051981838));
#30546=CARTESIAN_POINT('Ctrl Pts',(0.952834920914103,3.33178039838987,2.02784371169731));
#30547=CARTESIAN_POINT('Ctrl Pts',(-2.25562944112346,2.630740466173,2.18498222521083));
#30548=CARTESIAN_POINT('Ctrl Pts',(-3.43817673987435,-0.433127500149091,
2.34212073872434));
#30549=CARTESIAN_POINT('Ctrl Pts',(-1.53268946892128,-3.10797698807607,
2.49925925223786));
#30550=CARTESIAN_POINT('Ctrl Pts',(1.7493988709872,-2.99136460950407,2.65639776575137));
#30551=CARTESIAN_POINT('Ctrl Pts',(3.46024629894863,-0.188026617557356,
2.81353627926488));
#30552=CARTESIAN_POINT('Ctrl Pts',(2.06323722577413,2.78418938435949,2.97067479277839));
#30553=CARTESIAN_POINT('Ctrl Pts',(-1.18688998506621,3.25575653825361,3.12781330629191));
#30554=CARTESIAN_POINT('Ctrl Pts',(-3.3709995165217,0.803131807227777,3.28495181980542));
#30555=CARTESIAN_POINT('Ctrl Pts',(-2.52741049074122,-2.37083416635282,
3.44209033331894));
#30556=CARTESIAN_POINT('Ctrl Pts',(0.586198762341201,-3.41541058398195,
3.59922884683245));
#30557=CARTESIAN_POINT('Ctrl Pts',(3.17330745213002,-1.3924001776803,3.75636736034597));
#30558=CARTESIAN_POINT('Ctrl Pts',(2.91027678633445,1.88120904397026,3.91350587385948));
#30559=CARTESIAN_POINT('Ctrl Pts',(0.0333505152943699,3.46519064195013,
4.07064438737299));
#30560=CARTESIAN_POINT('Ctrl Pts',(-2.87352987075533,1.93687493734171,4.22778290088651));
#30561=CARTESIAN_POINT('Ctrl Pts',(-3.19951927885268,-1.33106529716661,
4.38492141440001));
#30562=CARTESIAN_POINT('Ctrl Pts',(-0.651826904677972,-3.40349528097662,
4.54205992791353));
#30563=CARTESIAN_POINT('Ctrl Pts',(2.48131063733581,-2.41904029776201,4.69919844142705));
#30564=CARTESIAN_POINT('Ctrl Pts',(3.38583301773356,0.738101088738959,4.85633695494055));
#30565=CARTESIAN_POINT('Ctrl Pts',(1.24933397805696,3.23230924456058,5.01347546845408));
#30566=CARTESIAN_POINT('Ctrl Pts',(-2.00926747133911,2.82338496663079,5.17061398196758));
#30567=CARTESIAN_POINT('Ctrl Pts',(-3.46322427730269,-0.12139211787978,
5.3277524954811));
#30568=CARTESIAN_POINT('Ctrl Pts',(-1.80664989208085,-2.95713959911133,
5.48489100899462));
#30569=CARTESIAN_POINT('Ctrl Pts',(1.47258603363221,-3.13690114838409,5.64202952250812));
#30570=CARTESIAN_POINT('Ctrl Pts',(3.4292033754596,-0.499222045701823,5.79916803602164));
#30571=CARTESIAN_POINT('Ctrl Pts',(2.30584575575073,2.58683857089803,5.95630654953515));
#30572=CARTESIAN_POINT('Ctrl Pts',(-0.888531402702859,3.34950300605675,
6.11344506304867));
#30573=CARTESIAN_POINT('Ctrl Pts',(-3.28486476693535,1.10377620199891,6.27058357656218));
#30574=CARTESIAN_POINT('Ctrl Pts',(-2.73086240406331,-2.13331876928079,
6.4277220900757));
#30575=CARTESIAN_POINT('Ctrl Pts',(0.275892655912234,-3.45435112336383,
6.5848606035892));
#30576=CARTESIAN_POINT('Ctrl Pts',(3.03485183459055,-1.67282180255638,6.74199911710273));
#30577=CARTESIAN_POINT('Ctrl Pts',(3.06802702248421,1.6111699572782,6.89913763061623));
#30578=CARTESIAN_POINT('Ctrl Pts',(0.345621576330127,3.44807252913389,7.05627614412975));
#30579=CARTESIAN_POINT('Ctrl Pts',(-2.68720751132516,2.18805261171336,7.21341465764325));
#30580=CARTESIAN_POINT('Ctrl Pts',(-3.30649300260574,-1.03718969811004,
7.37055317115678));
#30581=CARTESIAN_POINT('Ctrl Pts',(-0.956017138014702,-3.33086920560938,
7.52769168467029));
#30582=CARTESIAN_POINT('Ctrl Pts',(2.25311553735071,-2.63289362024357,7.68483019818381));
#30583=CARTESIAN_POINT('Ctrl Pts',(3.43858888024395,0.429842977951538,7.84196871169731));
#30584=CARTESIAN_POINT('Ctrl Pts',(1.53565755714059,3.10651158777771,7.99910722521083));
#30585=CARTESIAN_POINT('Ctrl Pts',(-1.74654067132524,2.99303427005181,8.15624573872433));
#30586=CARTESIAN_POINT('Ctrl Pts',(-3.46006514069016,0.191331803382343,
8.31338425223787));
#30587=CARTESIAN_POINT('Ctrl Pts',(-2.06589572612039,-2.78221724805058,
8.47052276575136));
#30588=CARTESIAN_POINT('Ctrl Pts',(1.183779392948,-3.25688886436581,8.62766127926489));
#30589=CARTESIAN_POINT('Ctrl Pts',(3.37023102179748,-0.806351310370959,
8.7847997927784));
#30590=CARTESIAN_POINT('Ctrl Pts',(2.52967359714463,2.36841856552378,8.94193830629191));
#30591=CARTESIAN_POINT('Ctrl Pts',(-0.582935293544439,3.41596954985013,
9.09907681980542));
#30592=CARTESIAN_POINT('Ctrl Pts',(-3.17197740603666,1.3954296219005,9.25621533331893));
#30593=CARTESIAN_POINT('Ctrl Pts',(-2.91206965945989,-1.87842613074489,
9.41335384683245));
#30594=CARTESIAN_POINT('Ctrl Pts',(-0.0366657672894424,-3.46516125435096,
9.57049236034596));
#30595=CARTESIAN_POINT('Ctrl Pts',(2.8716885037831,-1.93961114588268,9.72763087385947));
#30596=CARTESIAN_POINT('Ctrl Pts',(3.20077001198978,1.32799366090119,9.88476938737299));
#30597=CARTESIAN_POINT('Ctrl Pts',(0.655114493273841,3.40289939669598,10.0419079008865));
#30598=CARTESIAN_POINT('Ctrl Pts',(-2.47906919875826,2.42135526672317,10.1990464144));
#30599=CARTESIAN_POINT('Ctrl Pts',(-3.3864019310671,-0.734763106864168,
10.3561849279135));
#30600=CARTESIAN_POINT('Ctrl Pts',(-1.25267830620767,-3.23131219035953,
10.513323441427));
#30601=CARTESIAN_POINT('Ctrl Pts',(2.00706204302524,-2.82492459714601,10.6704619549406));
#30602=CARTESIAN_POINT('Ctrl Pts',(3.46239353138226,0.117358798249391,10.8276004684541));
#30603=CARTESIAN_POINT('Ctrl Pts',(1.81131357477516,2.9568147670617,10.9847389819676));
#30604=CARTESIAN_POINT('Ctrl Pts',(-1.47339811761136,3.13548357068097,11.1418774954811));
#30605=CARTESIAN_POINT('Ctrl Pts',(-2.77050414434575,1.38461669033425,11.2466365044901));
#30606=CARTESIAN_POINT('Ctrl Pts',(-2.91090525077877,0.426608275808828,
11.2990160089946));
#30607=CARTESIAN_POINT('Ctrl Pts',(1.59774743137964,-2.24059110187414,-0.219489327336925));
#30608=CARTESIAN_POINT('Ctrl Pts',(2.33514866714022,-1.71475623207252,-0.167109822832421));
#30609=CARTESIAN_POINT('Ctrl Pts',(3.23863136773739,0.11226788144075,-0.0623508138234118));
#30610=CARTESIAN_POINT('Ctrl Pts',(1.6876604910601,2.76982094937113,0.0947876996901019));
#30611=CARTESIAN_POINT('Ctrl Pts',(-1.38044412748324,2.93181193130462,0.251926213203615));
#30612=CARTESIAN_POINT('Ctrl Pts',(-3.2079816177237,0.464474356210045,0.409064726717129));
#30613=CARTESIAN_POINT('Ctrl Pts',(-2.15460694798876,-2.42206010021071,
0.566203240230643));
#30614=CARTESIAN_POINT('Ctrl Pts',(0.834144210720117,-3.13213929648004,
0.723341753744155));
#30615=CARTESIAN_POINT('Ctrl Pts',(3.07359869399491,-1.02960715343621,0.880480267257669));
#30616=CARTESIAN_POINT('Ctrl Pts',(2.55252127926951,1.99796636155783,1.03761878077118));
#30617=CARTESIAN_POINT('Ctrl Pts',(-0.261157599233816,3.2308943271893,1.19475729428469));
#30618=CARTESIAN_POINT('Ctrl Pts',(-2.84026054414775,1.56203972461538,1.35189580779821));
#30619=CARTESIAN_POINT('Ctrl Pts',(-2.86836128896387,-1.50981857631063,
1.50903432131172));
#30620=CARTESIAN_POINT('Ctrl Pts',(-0.320209305227662,-3.22559586930712,
1.66617283482524));
#30621=CARTESIAN_POINT('Ctrl Pts',(2.51553994814305,-2.04428172839443,1.82331134833875));
#30622=CARTESIAN_POINT('Ctrl Pts',(3.09193171078347,0.973131394588079,1.98044986185226));
#30623=CARTESIAN_POINT('Ctrl Pts',(0.891272025644291,3.1165132590083,2.13758837536578));
#30624=CARTESIAN_POINT('Ctrl Pts',(-2.10989267602029,2.4607676867899,2.29472688887929));
#30625=CARTESIAN_POINT('Ctrl Pts',(-3.21603530707201,-0.405143027346019,
2.4518654023928));
#30626=CARTESIAN_POINT('Ctrl Pts',(-1.43366203071003,-2.90716984129947,
2.60900391590632));
#30627=CARTESIAN_POINT('Ctrl Pts',(1.63636978576396,-2.79809181678146,2.76614242941983));
#30628=CARTESIAN_POINT('Ctrl Pts',(3.23667894658341,-0.175878172207005,
2.92328094293335));
#30629=CARTESIAN_POINT('Ctrl Pts',(1.92993096835312,2.60430223316632,3.08041945644686));
#30630=CARTESIAN_POINT('Ctrl Pts',(-1.11020473535129,3.04540131890859,3.23755796996037));
#30631=CARTESIAN_POINT('Ctrl Pts',(-3.15319842040834,0.751241266431068,
3.39469648347389));
#30632=CARTESIAN_POINT('Ctrl Pts',(-2.36411388612472,-2.21765399601942,
3.5518349969874));
#30633=CARTESIAN_POINT('Ctrl Pts',(0.548324318173406,-3.19474007803184,
3.70897351050091));
#30634=CARTESIAN_POINT('Ctrl Pts',(2.96827928823051,-1.30243686459143,3.86611202401443));
#30635=CARTESIAN_POINT('Ctrl Pts',(2.72224309752783,1.75966367151117,4.02325053752794));
#30636=CARTESIAN_POINT('Ctrl Pts',(0.0311957304148393,3.24130383438475,
4.18038905104146));
#30637=CARTESIAN_POINT('Ctrl Pts',(-2.68787040907414,1.81173297801481,4.33752756455496));
#30638=CARTESIAN_POINT('Ctrl Pts',(-2.99279756247315,-1.24506484557935,
4.49466607806848));
#30639=CARTESIAN_POINT('Ctrl Pts',(-0.609712210321215,-3.18359462564273,
4.65180459158199));
#30640=CARTESIAN_POINT('Ctrl Pts',(2.32099255542547,-2.26274551758992,4.80894310509551));
#30641=CARTESIAN_POINT('Ctrl Pts',(3.16707352551029,0.69041219843154,4.96608161860902));
#30642=CARTESIAN_POINT('Ctrl Pts',(1.16861420681437,3.02346896054623,5.12322013212254));
#30643=CARTESIAN_POINT('Ctrl Pts',(-1.87944821283798,2.64096537936348,5.28035864563605));
#30644=CARTESIAN_POINT('Ctrl Pts',(-3.23946451703395,-0.113548943710187,
5.43749715914956));
#30645=CARTESIAN_POINT('Ctrl Pts',(-1.68992180450333,-2.76607809260859,
5.59463567266307));
#30646=CARTESIAN_POINT('Ctrl Pts',(1.37744189294803,-2.93422520459686,5.75177418617659));
#30647=CARTESIAN_POINT('Ctrl Pts',(3.20764171390784,-0.466967188284919,
5.9089126996901));
#30648=CARTESIAN_POINT('Ctrl Pts',(2.15686450238375,2.41970230361335,6.06605121320362));
#30649=CARTESIAN_POINT('Ctrl Pts',(-0.831123173336083,3.13309080469669,
6.22318972671712));
#30650=CARTESIAN_POINT('Ctrl Pts',(-3.07262885787747,1.03246095396017,6.38032824023064));
#30651=CARTESIAN_POINT('Ctrl Pts',(-2.55442072199701,-1.99548452634149,
6.53746675374416));
#30652=CARTESIAN_POINT('Ctrl Pts',(0.258067164519323,-3.23116465972251,
6.69460526725767));
#30653=CARTESIAN_POINT('Ctrl Pts',(2.83876932171097,-1.56474038029172,6.85174378077119));
#30654=CARTESIAN_POINT('Ctrl Pts',(2.86980105267096,1.50707187568543,7.00888229428469));
#30655=CARTESIAN_POINT('Ctrl Pts',(0.323290882482136,3.22529172698812,7.1660208077982));
#30656=CARTESIAN_POINT('Ctrl Pts',(-2.51358638246349,2.04668200194341,7.32315932131173));
#30657=CARTESIAN_POINT('Ctrl Pts',(-3.09285968799709,-0.970176620232505,
7.48029783482524));
#30658=CARTESIAN_POINT('Ctrl Pts',(-0.89424863892644,-3.11566093861428,
7.63743634833875));
#30659=CARTESIAN_POINT('Ctrl Pts',(2.10754119617984,-2.46278172505391,7.79457486185227));
#30660=CARTESIAN_POINT('Ctrl Pts',(3.21642081895241,0.402070718924034,7.95171337536577));
#30661=CARTESIAN_POINT('Ctrl Pts',(1.43643835002984,2.90579912086969,8.1088518888793));
#30662=CARTESIAN_POINT('Ctrl Pts',(-1.63369625507517,2.79965360015637,8.2659904023928));
#30663=CARTESIAN_POINT('Ctrl Pts',(-3.23650949300394,0.178969809174445,
8.42312891590632));
#30664=CARTESIAN_POINT('Ctrl Pts',(-1.93241770234741,-2.6024575170625,8.58026742941983));
#30665=CARTESIAN_POINT('Ctrl Pts',(1.10729511934404,-3.04646048515613,8.73740594293334));
#30666=CARTESIAN_POINT('Ctrl Pts',(3.15247957831459,-0.75425275669555,8.89454445644686));
#30667=CARTESIAN_POINT('Ctrl Pts',(2.36623077267467,2.21539446774564,9.05168296996036));
#30668=CARTESIAN_POINT('Ctrl Pts',(-0.54527170288688,3.19526292897974,9.20882148347389));
#30669=CARTESIAN_POINT('Ctrl Pts',(-2.96703517673773,1.30527057568604,9.36595999698739));
#30670=CARTESIAN_POINT('Ctrl Pts',(-2.72392013268591,-1.75706056298405,
9.52309851050092));
#30671=CARTESIAN_POINT('Ctrl Pts',(-0.0342967831746755,-3.24127634552548,
9.68023702401442));
#30672=CARTESIAN_POINT('Ctrl Pts',(2.68614801326846,-1.81429239945851,9.83737553752795));
#30673=CARTESIAN_POINT('Ctrl Pts',(2.99396748543899,1.24219166847781,9.99451405104144));
#30674=CARTESIAN_POINT('Ctrl Pts',(0.612787387020777,3.18303724158995,10.151652564555));
#30675=CARTESIAN_POINT('Ctrl Pts',(-2.31889593673789,2.2649109158452,10.3087910780685));
#30676=CARTESIAN_POINT('Ctrl Pts',(-3.16760568121541,-0.687289884375024,
10.465929591582));
#30677=CARTESIAN_POINT('Ctrl Pts',(-1.17174245711238,-3.02253632625886,
10.6230681050955));
#30678=CARTESIAN_POINT('Ctrl Pts',(1.8773852777822,-2.64240553397781,10.780206618609));
#30679=CARTESIAN_POINT('Ctrl Pts',(3.23868744580887,0.109776217839061,10.9373451321225));
#30680=CARTESIAN_POINT('Ctrl Pts',(1.69428416552798,2.76577424803644,11.0944836456361));
#30681=CARTESIAN_POINT('Ctrl Pts',(-1.37820150798437,2.93289921693286,11.2516221591496));
#30682=CARTESIAN_POINT('Ctrl Pts',(-2.59150119982806,1.29515627025004,11.3563811681586));
#30683=CARTESIAN_POINT('Ctrl Pts',(-2.72283095673203,0.399045011671044,
11.4087606726631));
#30684=CARTESIAN_POINT('Ctrl Pts',(1.48738611075532,-2.08582659521589,-0.109744663668464));
#30685=CARTESIAN_POINT('Ctrl Pts',(2.17385277913045,-1.59631275433404,-0.0573651591639592));
#30686=CARTESIAN_POINT('Ctrl Pts',(3.01492915564857,0.104513194175331,0.0473938498450494));
#30687=CARTESIAN_POINT('Ctrl Pts',(1.57108859934498,2.57850091226017,0.204532363358563));
#30688=CARTESIAN_POINT('Ctrl Pts',(-1.28509261324199,2.72930267971312,0.361670876872076));
#30689=CARTESIAN_POINT('Ctrl Pts',(-2.98639647797178,0.432391686358259,
0.51880939038559));
#30690=CARTESIAN_POINT('Ctrl Pts',(-2.00578163083517,-2.25476097267596,
0.675947903899103));
#30691=CARTESIAN_POINT('Ctrl Pts',(0.776527309025778,-2.9157928187139,0.833086417412617));
#30692=CARTESIAN_POINT('Ctrl Pts',(2.86129579537873,-0.958489026161636,
0.99022493092613));
#30693=CARTESIAN_POINT('Ctrl Pts',(2.37621079754423,1.85996069064019,1.14736344443964));
#30694=CARTESIAN_POINT('Ctrl Pts',(-0.243118642026661,3.00772653624605,
1.30450195795316));
#30695=CARTESIAN_POINT('Ctrl Pts',(-2.64407502795598,1.45414484493007,1.46164047146667));
#30696=CARTESIAN_POINT('Ctrl Pts',(-2.67023476805036,-1.40553077167252,
1.61877898498018));
#30697=CARTESIAN_POINT('Ctrl Pts',(-0.298091465381954,-3.00279405911757,
1.7759174984937));
#30698=CARTESIAN_POINT('Ctrl Pts',(2.34178388050189,-1.90307691288803,1.93305601200721));
#30699=CARTESIAN_POINT('Ctrl Pts',(2.87836249441012,0.905914221373807,2.09019452552073));
#30700=CARTESIAN_POINT('Ctrl Pts',(0.829709130374474,2.90124611962672,2.24733303903424));
#30701=CARTESIAN_POINT('Ctrl Pts',(-1.96415591091712,2.2907949074068,2.40447155254775));
#30702=CARTESIAN_POINT('Ctrl Pts',(-2.99389387426969,-0.37715855454295,
2.56161006606126));
#30703=CARTESIAN_POINT('Ctrl Pts',(-1.33463459249878,-2.70636269452286,
2.71874857957478));
#30704=CARTESIAN_POINT('Ctrl Pts',(1.52334070054072,-2.60481902405885,2.87588709308829));
#30705=CARTESIAN_POINT('Ctrl Pts',(3.01311159421818,-0.163729726856653,
3.03302560660181));
#30706=CARTESIAN_POINT('Ctrl Pts',(1.79662471093212,2.42441508197314,3.19016412011532));
#30707=CARTESIAN_POINT('Ctrl Pts',(-1.03351948563637,2.83504609956357,3.34730263362884));
#30708=CARTESIAN_POINT('Ctrl Pts',(-2.93539732429499,0.699350725634357,
3.50444114714234));
#30709=CARTESIAN_POINT('Ctrl Pts',(-2.20081728150821,-2.06447382568602,
3.66157966065586));
#30710=CARTESIAN_POINT('Ctrl Pts',(0.510449874005612,-2.97406957208172,
3.81871817416937));
#30711=CARTESIAN_POINT('Ctrl Pts',(2.763251124331,-1.21247355150257,3.97585668768289));
#30712=CARTESIAN_POINT('Ctrl Pts',(2.5342094087212,1.63811829905208,4.1329952011964));
#30713=CARTESIAN_POINT('Ctrl Pts',(0.029040945535309,3.01741702681936,4.29013371470992));
#30714=CARTESIAN_POINT('Ctrl Pts',(-2.50221094739296,1.68659101868791,4.44727222822342));
#30715=CARTESIAN_POINT('Ctrl Pts',(-2.78607584609361,-1.1590643939921,4.60441074173694));
#30716=CARTESIAN_POINT('Ctrl Pts',(-0.56759751596446,-2.96369397030884,
4.76154925525046));
#30717=CARTESIAN_POINT('Ctrl Pts',(2.16067447351513,-2.10645073741783,4.91868776876396));
#30718=CARTESIAN_POINT('Ctrl Pts',(2.94831403328702,0.642723308124124,5.07582628227749));
#30719=CARTESIAN_POINT('Ctrl Pts',(1.08789443557179,2.81462867653188,5.23296479579099));
#30720=CARTESIAN_POINT('Ctrl Pts',(-1.74962895433684,2.45854579209617,5.39010330930451));
#30721=CARTESIAN_POINT('Ctrl Pts',(-3.01570475676522,-0.105705769540595,
5.54724182281802));
#30722=CARTESIAN_POINT('Ctrl Pts',(-1.57319371692581,-2.57501658610585,
5.70438033633154));
#30723=CARTESIAN_POINT('Ctrl Pts',(1.28229775226384,-2.73154926080963,5.86151884984505));
#30724=CARTESIAN_POINT('Ctrl Pts',(2.98608005235609,-0.434712330868017,
6.01865736335856));
#30725=CARTESIAN_POINT('Ctrl Pts',(2.00788324901678,2.25256603632868,6.17579587687208));
#30726=CARTESIAN_POINT('Ctrl Pts',(-0.773714943969305,2.91667860333663,
6.33293439038559));
#30727=CARTESIAN_POINT('Ctrl Pts',(-2.86039294881959,0.961145705921419,
6.4900729038991));
#30728=CARTESIAN_POINT('Ctrl Pts',(-2.37797903993071,-1.85765028340219,
6.64721141741262));
#30729=CARTESIAN_POINT('Ctrl Pts',(0.240241673126412,-3.0079781960812,6.80434993092612));
#30730=CARTESIAN_POINT('Ctrl Pts',(2.64268680883139,-1.45665895802706,6.96148844443965));
#30731=CARTESIAN_POINT('Ctrl Pts',(2.67157508285772,1.40297379409266,7.11862695795316));
#30732=CARTESIAN_POINT('Ctrl Pts',(0.300960188634146,3.00251092484234,7.27576547146667));
#30733=CARTESIAN_POINT('Ctrl Pts',(-2.33996525360183,1.90531139217345,7.43290398498018));
#30734=CARTESIAN_POINT('Ctrl Pts',(-2.87922637338843,-0.903163542354968,
7.5900424984937));
#30735=CARTESIAN_POINT('Ctrl Pts',(-0.832480139838179,-2.90045267161919,
7.74718101200721));
#30736=CARTESIAN_POINT('Ctrl Pts',(1.96196685500896,-2.29266982986425,7.90431952552073));
#30737=CARTESIAN_POINT('Ctrl Pts',(2.99425275766087,0.37429845989653,8.06145803903424));
#30738=CARTESIAN_POINT('Ctrl Pts',(1.33721914291908,2.70508665396167,8.21859655254775));
#30739=CARTESIAN_POINT('Ctrl Pts',(-1.5208518388251,2.60627293026094,8.37573506606126));
#30740=CARTESIAN_POINT('Ctrl Pts',(-3.01295384531772,0.166607814966547,
8.53287357957478));
#30741=CARTESIAN_POINT('Ctrl Pts',(-1.79893967857444,-2.42269778607442,
8.69001209308829));
#30742=CARTESIAN_POINT('Ctrl Pts',(1.03081084574009,-2.83603210594645,8.8471506066018));
#30743=CARTESIAN_POINT('Ctrl Pts',(2.9347281348317,-0.702154203020143,9.00428912011532));
#30744=CARTESIAN_POINT('Ctrl Pts',(2.20278794820472,2.06237036996751,9.16142763362883));
#30745=CARTESIAN_POINT('Ctrl Pts',(-0.507608112229325,2.97455630810935,
9.31856614714235));
#30746=CARTESIAN_POINT('Ctrl Pts',(-2.7620929474388,1.21511152947157,9.47570466065586));
#30747=CARTESIAN_POINT('Ctrl Pts',(-2.53577060591194,-1.63569499522321,
9.63284317416937));
#30748=CARTESIAN_POINT('Ctrl Pts',(-0.0319277990599106,-3.0173914367,9.78998168768289));
#30749=CARTESIAN_POINT('Ctrl Pts',(2.50060752275382,-1.68897365303435,9.94712020119639));
#30750=CARTESIAN_POINT('Ctrl Pts',(2.78716495888821,1.15638967605443,10.1042587147099));
#30751=CARTESIAN_POINT('Ctrl Pts',(0.570460280767717,2.96317508648391,10.2613972282234));
#30752=CARTESIAN_POINT('Ctrl Pts',(-2.15872267471752,2.10846656496723,10.4185357417369));
#30753=CARTESIAN_POINT('Ctrl Pts',(-2.94880943136371,-0.639816661885883,
10.5756742552505));
#30754=CARTESIAN_POINT('Ctrl Pts',(-1.09080660801709,-2.8137604621582,10.732812768764));
#30755=CARTESIAN_POINT('Ctrl Pts',(1.74770851253917,-2.4598864708096,10.8899512822775));
#30756=CARTESIAN_POINT('Ctrl Pts',(3.01498136023548,0.102193637428725,11.047089795791));
#30757=CARTESIAN_POINT('Ctrl Pts',(1.57725475628079,2.57473372901119,11.2042283093045));
#30758=CARTESIAN_POINT('Ctrl Pts',(-1.28300489835739,2.73031486318474,11.361366822818));
#30759=CARTESIAN_POINT('Ctrl Pts',(-2.41249825531037,1.20569585016584,11.466125831827));
#30760=CARTESIAN_POINT('Ctrl Pts',(-2.53475666268528,0.371481747533259,
11.5185053363315));
#30761=CARTESIAN_POINT('Ctrl Pts',(1.37702479013101,-1.93106208855765,-2.4980018054066E-15));
#30762=CARTESIAN_POINT('Ctrl Pts',(2.01255689112068,-1.47786927659557,0.052379504504502));
#30763=CARTESIAN_POINT('Ctrl Pts',(2.79122694355976,0.0967585069099138,
0.157138513513511));
#30764=CARTESIAN_POINT('Ctrl Pts',(1.45451670762985,2.3871808751492,0.314277027027025));
#30765=CARTESIAN_POINT('Ctrl Pts',(-1.18974109900074,2.52679342812162,0.471415540540538));
#30766=CARTESIAN_POINT('Ctrl Pts',(-2.76481133821986,0.40030901650647,0.628554054054051));
#30767=CARTESIAN_POINT('Ctrl Pts',(-1.85695631368159,-2.0874618451412,0.785692567567565));
#30768=CARTESIAN_POINT('Ctrl Pts',(0.718910407331439,-2.69944634094777,
0.942831081081078));
#30769=CARTESIAN_POINT('Ctrl Pts',(2.64899289676255,-0.887370898887054,
1.09996959459459));
#30770=CARTESIAN_POINT('Ctrl Pts',(2.19990031581894,1.72195501972256,1.25710810810811));
#30771=CARTESIAN_POINT('Ctrl Pts',(-0.225079684819506,2.78455874530281,
1.41424662162162));
#30772=CARTESIAN_POINT('Ctrl Pts',(-2.44788951176421,1.34624996524475,1.57138513513514));
#30773=CARTESIAN_POINT('Ctrl Pts',(-2.47210824713685,-1.30124296703442,
1.72852364864864));
#30774=CARTESIAN_POINT('Ctrl Pts',(-0.275973625536248,-2.77999224892802,
1.88566216216216));
#30775=CARTESIAN_POINT('Ctrl Pts',(2.16802781286073,-1.76187209738162,2.04280067567567));
#30776=CARTESIAN_POINT('Ctrl Pts',(2.66479327803676,0.838697048159531,2.19993918918919));
#30777=CARTESIAN_POINT('Ctrl Pts',(0.76814623510466,2.68597898024514,2.3570777027027));
#30778=CARTESIAN_POINT('Ctrl Pts',(-1.81841914581395,2.1208221280237,2.51421621621621));
#30779=CARTESIAN_POINT('Ctrl Pts',(-2.77175244146736,-0.349174081739879,
2.67135472972972));
#30780=CARTESIAN_POINT('Ctrl Pts',(-1.23560715428754,-2.50555554774625,
2.82849324324324));
#30781=CARTESIAN_POINT('Ctrl Pts',(1.41031161531747,-2.41154623133624,2.98563175675675));
#30782=CARTESIAN_POINT('Ctrl Pts',(2.78954424185296,-0.151581281506301,
3.14277027027027));
#30783=CARTESIAN_POINT('Ctrl Pts',(1.66331845351111,2.24452793077997,3.29990878378378));
#30784=CARTESIAN_POINT('Ctrl Pts',(-0.956834235921451,2.62469088021855,
3.45704729729729));
#30785=CARTESIAN_POINT('Ctrl Pts',(-2.71759622818163,0.647460184837647,
3.61418581081081));
#30786=CARTESIAN_POINT('Ctrl Pts',(-2.03752067689171,-1.91129365535261,
3.77132432432432));
#30787=CARTESIAN_POINT('Ctrl Pts',(0.47257542983782,-2.75339906613161,3.92846283783783));
#30788=CARTESIAN_POINT('Ctrl Pts',(2.55822296043148,-1.12251023841371,4.08560135135135));
#30789=CARTESIAN_POINT('Ctrl Pts',(2.34617571991457,1.51657292659299,4.24273986486486));
#30790=CARTESIAN_POINT('Ctrl Pts',(0.0268861606557786,2.79353021925399,
4.39987837837838));
#30791=CARTESIAN_POINT('Ctrl Pts',(-2.31655148571177,1.56144905936101,4.55701689189189));
#30792=CARTESIAN_POINT('Ctrl Pts',(-2.57935412971408,-1.07306394240484,
4.7141554054054));
#30793=CARTESIAN_POINT('Ctrl Pts',(-0.525482821607704,-2.74379331497496,
4.87129391891892));
#30794=CARTESIAN_POINT('Ctrl Pts',(2.00035639160479,-1.95015595724574,5.02843243243243));
#30795=CARTESIAN_POINT('Ctrl Pts',(2.72955454106374,0.595034417816705,5.18557094594594));
#30796=CARTESIAN_POINT('Ctrl Pts',(1.0071746643292,2.60578839251754,5.34270945945947));
#30797=CARTESIAN_POINT('Ctrl Pts',(-1.61980969583571,2.27612620482886,5.49984797297296));
#30798=CARTESIAN_POINT('Ctrl Pts',(-2.79194499649648,-0.0978625953710016,
5.6569864864865));
#30799=CARTESIAN_POINT('Ctrl Pts',(-1.45646562934828,-2.38395507960311,
5.81412499999999));
#30800=CARTESIAN_POINT('Ctrl Pts',(1.18715361157964,-2.5288733170224,5.97126351351352));
#30801=CARTESIAN_POINT('Ctrl Pts',(2.76451839080433,-0.402457473451116,
6.12840202702702));
#30802=CARTESIAN_POINT('Ctrl Pts',(1.8589019956498,2.08542976904401,6.28554054054054));
#30803=CARTESIAN_POINT('Ctrl Pts',(-0.716306714602523,2.70026640197657,
6.44267905405405));
#30804=CARTESIAN_POINT('Ctrl Pts',(-2.64815703976171,0.889830457882673,
6.59981756756756));
#30805=CARTESIAN_POINT('Ctrl Pts',(-2.20153735786441,-1.71981604046289,
6.75695608108108));
#30806=CARTESIAN_POINT('Ctrl Pts',(0.222416181733502,-2.78479173243988,
6.91409459459459));
#30807=CARTESIAN_POINT('Ctrl Pts',(2.4466042959518,-1.34857753576241,7.0712331081081));
#30808=CARTESIAN_POINT('Ctrl Pts',(2.47334911304448,1.29887571249989,7.22837162162162));
#30809=CARTESIAN_POINT('Ctrl Pts',(0.278629494786153,2.77973012269657,7.38551013513513));
#30810=CARTESIAN_POINT('Ctrl Pts',(-2.16634412474015,1.76394078240349,7.54264864864865));
#30811=CARTESIAN_POINT('Ctrl Pts',(-2.66559305877978,-0.83615046447743,
7.69978716216215));
#30812=CARTESIAN_POINT('Ctrl Pts',(-0.770711640749916,-2.68524440462409,
7.85692567567567));
#30813=CARTESIAN_POINT('Ctrl Pts',(1.81639251383808,-2.12255793467458,8.01406418918919));
#30814=CARTESIAN_POINT('Ctrl Pts',(2.77208469636934,0.346526200869026,8.1712027027027));
#30815=CARTESIAN_POINT('Ctrl Pts',(1.23799993580832,2.50437418705365,8.32834121621622));
#30816=CARTESIAN_POINT('Ctrl Pts',(-1.40800742257503,2.4128922603655,8.48547972972973));
#30817=CARTESIAN_POINT('Ctrl Pts',(-2.78939819763151,0.154245820758651,
8.64261824324324));
#30818=CARTESIAN_POINT('Ctrl Pts',(-1.66546165480147,-2.24293805508635,
8.79975675675676));
#30819=CARTESIAN_POINT('Ctrl Pts',(0.954326572136137,-2.62560372673677,
8.95689527027026));
#30820=CARTESIAN_POINT('Ctrl Pts',(2.71697669134881,-0.650055649344734,
9.11403378378378));
#30821=CARTESIAN_POINT('Ctrl Pts',(2.03934512373477,1.90934627218937,9.2711722972973));
#30822=CARTESIAN_POINT('Ctrl Pts',(-0.469944521571767,2.75384968723896,
9.42831081081079));
#30823=CARTESIAN_POINT('Ctrl Pts',(-2.55715071813987,1.12495248325711,9.58544932432433));
#30824=CARTESIAN_POINT('Ctrl Pts',(-2.34762107913798,-1.51432942746238,
9.74258783783783));
#30825=CARTESIAN_POINT('Ctrl Pts',(-0.0295588149451427,-2.79350652787453,
9.89972635135136));
#30826=CARTESIAN_POINT('Ctrl Pts',(2.31506703223917,-1.56365490661018,10.0568648648649));
#30827=CARTESIAN_POINT('Ctrl Pts',(2.58036243233743,1.07058768363104,10.2140033783784));
#30828=CARTESIAN_POINT('Ctrl Pts',(0.528133174514654,2.74331293137788,10.3711418918919));
#30829=CARTESIAN_POINT('Ctrl Pts',(-1.99854941269714,1.95202221408926,10.5282804054054));
#30830=CARTESIAN_POINT('Ctrl Pts',(-2.73001318151202,-0.59234343939674,
10.6854189189189));
#30831=CARTESIAN_POINT('Ctrl Pts',(-1.0098707589218,-2.60498459805753,10.8425574324324));
#30832=CARTESIAN_POINT('Ctrl Pts',(1.61803174729613,-2.2773674076414,10.999695945946));
#30833=CARTESIAN_POINT('Ctrl Pts',(2.79127527466209,0.0946110570183949,
11.1568344594594));
#30834=CARTESIAN_POINT('Ctrl Pts',(1.46022534703361,2.38369320998594,11.313972972973));
#30835=CARTESIAN_POINT('Ctrl Pts',(-1.1878082887304,2.52773050943662,11.4711114864865));
#30836=CARTESIAN_POINT('Ctrl Pts',(-2.23349531079268,1.11623543008163,11.5758704954955));
#30837=CARTESIAN_POINT('Ctrl Pts',(-2.34668236863853,0.343918483395475,
11.62825));
#30838=CARTESIAN_POINT('',(1.37702479013102,-1.93106208855765,0.));
#30839=CARTESIAN_POINT('Ctrl Pts',(1.37702479013101,-1.93106208855765,-2.4980018054066E-15));
#30840=CARTESIAN_POINT('Ctrl Pts',(2.01255689112068,-1.47786927659557,0.052379504504502));
#30841=CARTESIAN_POINT('Ctrl Pts',(2.79122694355976,0.0967585069099138,
0.157138513513511));
#30842=CARTESIAN_POINT('Ctrl Pts',(1.45451670762985,2.3871808751492,0.314277027027025));
#30843=CARTESIAN_POINT('Ctrl Pts',(-1.18974109900074,2.52679342812162,0.471415540540538));
#30844=CARTESIAN_POINT('Ctrl Pts',(-2.31615344009055,1.00603694073732,0.583793234229858));
#30845=CARTESIAN_POINT('Ctrl Pts',(-2.37458477423974,0.11510370689526,0.643791423414673));
#30846=CARTESIAN_POINT('Ctrl Pts',(-2.37366757034868,0.001844716469488,
0.651410108094984));
#30847=CARTESIAN_POINT('Ctrl Pts',(1.29197400994444,2.64783394680711,-2.46330733588707E-16));
#30848=CARTESIAN_POINT('Ctrl Pts',(1.37074936016223,2.60046826619745,-2.90204607120186E-16));
#30849=CARTESIAN_POINT('Ctrl Pts',(1.44700091320012,2.54930204226795,-5.92854700626308E-16));
#30850=CARTESIAN_POINT('Ctrl Pts',(1.5204041597113,2.49432533414619,-4.68375338513738E-16));
#30851=CARTESIAN_POINT('Ctrl Pts',(1.59876972116939,2.43563200920691,-3.1748808003354E-16));
#30852=CARTESIAN_POINT('Ctrl Pts',(1.67388955782072,2.37259497158855,9.42702435984343E-17));
#30853=CARTESIAN_POINT('Ctrl Pts',(1.74558455766593,2.30559334150577,2.91433543964104E-16));
#30854=CARTESIAN_POINT('Ctrl Pts',(1.78514524738377,2.26862241321206,4.00226572297347E-16));
#30855=CARTESIAN_POINT('Ctrl Pts',(1.82366240526687,2.23044382157621,2.41712413072573E-16));
#30856=CARTESIAN_POINT('Ctrl Pts',(1.86109995619813,2.19111823230724,2.56739074444567E-16));
#30857=CARTESIAN_POINT('Ctrl Pts',(1.87813922122651,2.17321964863167,2.63578284255041E-16));
#30858=CARTESIAN_POINT('Ctrl Pts',(1.89495840460327,2.15507923207588,-5.32738877742354E-17));
#30859=CARTESIAN_POINT('Ctrl Pts',(1.91153266312519,2.13672660521873,-9.0205620750794E-17));
#30860=CARTESIAN_POINT('Ctrl Pts',(1.97664662778045,2.0646261070319,-2.35296368099375E-16));
#30861=CARTESIAN_POINT('Ctrl Pts',(2.03804038590891,1.98919650283574,-3.72373475267393E-16));
#30862=CARTESIAN_POINT('Ctrl Pts',(2.09554796148623,1.91081666271006,-8.32667268468867E-17));
#30863=CARTESIAN_POINT('Ctrl Pts',(2.14343533270609,1.8455486617107,1.57476549926517E-16));
#30864=CARTESIAN_POINT('Ctrl Pts',(2.18862729734747,1.77823406218829,2.53857300975798E-16));
#30865=CARTESIAN_POINT('Ctrl Pts',(2.23100237945407,1.70908145885149,3.19189119579733E-16));
#30866=CARTESIAN_POINT('Ctrl Pts',(2.2495414778757,1.67882719489164,3.47771790218954E-16));
#30867=CARTESIAN_POINT('Ctrl Pts',(2.26754109313608,1.64822104628506,2.94521883274651E-16));
#30868=CARTESIAN_POINT('Ctrl Pts',(2.28498954152194,1.61728023964544,3.19189119579733E-16));
#30869=CARTESIAN_POINT('Ctrl Pts',(2.29543189661598,1.59876312668031,3.33951695310829E-16));
#30870=CARTESIAN_POINT('Ctrl Pts',(2.30567682494647,1.58012614919259,-6.61366324171955E-18));
#30871=CARTESIAN_POINT('Ctrl Pts',(2.31572165746038,1.56137299470242,-1.38777878078145E-17));
#30872=CARTESIAN_POINT('Ctrl Pts',(2.32292320728395,1.54792809393149,-1.90857347710862E-17));
#30873=CARTESIAN_POINT('Ctrl Pts',(2.33002152872364,1.53442403232929,-1.12870283643031E-16));
#30874=CARTESIAN_POINT('Ctrl Pts',(2.33700969851763,1.52087413145422,-1.11022302462516E-16));
#30875=CARTESIAN_POINT('Ctrl Pts',(2.38058260792534,1.43638725996736,-9.94996979838631E-17));
#30876=CARTESIAN_POINT('Ctrl Pts',(2.41994184512486,1.3499998824768,-3.77842799305168E-16));
#30877=CARTESIAN_POINT('Ctrl Pts',(2.45492973401008,1.26206183108408,-3.7470027081099E-16));
#30878=CARTESIAN_POINT('Ctrl Pts',(2.48961375478266,1.17488751738912,-3.71585035023886E-16));
#30879=CARTESIAN_POINT('Ctrl Pts',(2.52000223755862,1.08618841594484,-4.13121512185277E-16));
#30880=CARTESIAN_POINT('Ctrl Pts',(2.54589150534161,0.996296170221892,-3.7470027081099E-16));
#30881=CARTESIAN_POINT('Ctrl Pts',(2.57095558696702,0.909269120898709,-3.37503655671981E-16));
#30882=CARTESIAN_POINT('Ctrl Pts',(2.59180267862827,0.821123009321661,-1.98135956264892E-16));
#30883=CARTESIAN_POINT('Ctrl Pts',(2.60819974692058,0.732162501184589,-2.77555756156289E-16));
#30884=CARTESIAN_POINT('Ctrl Pts',(2.61796168819389,0.679200152025794,-3.24838075693952E-16));
#30885=CARTESIAN_POINT('Ctrl Pts',(2.62614545111416,0.625949276096869,-2.51374357035676E-17));
#30886=CARTESIAN_POINT('Ctrl Pts',(2.63269335080009,0.572476447093945,0.));
#30887=CARTESIAN_POINT('Ctrl Pts',(2.6352683765624,0.5514477327168,9.88554309620052E-18));
#30888=CARTESIAN_POINT('Ctrl Pts',(2.63759088070415,0.530377846603737,-5.43523939458827E-17));
#30889=CARTESIAN_POINT('Ctrl Pts',(2.63965388200594,0.50930758122065,-2.77555756156289E-17));
#30890=CARTESIAN_POINT('Ctrl Pts',(2.64834931960739,0.420497565576959,8.43485582923526E-17));
#30891=CARTESIAN_POINT('Ctrl Pts',(2.65245297898025,0.3315870178655,7.13394232030532E-17));
#30892=CARTESIAN_POINT('Ctrl Pts',(2.65178792227632,0.242870082265014,1.11022302462516E-16));
#30893=CARTESIAN_POINT('Ctrl Pts',(2.65141677862428,0.193360428001277,1.33167855834344E-16));
#30894=CARTESIAN_POINT('Ctrl Pts',(2.64955959473733,0.143911103160085,2.55410202784461E-16));
#30895=CARTESIAN_POINT('Ctrl Pts',(2.64617859082989,0.0945743399740305,
2.77555756156289E-16));
#30896=CARTESIAN_POINT('Ctrl Pts',(2.63998980161557,0.00426541509996067,
2.91350122435194E-16));
#30897=CARTESIAN_POINT('Ctrl Pts',(2.62869784498548,-0.0856678806083358,
1.22336690906674E-16));
#30898=CARTESIAN_POINT('Ctrl Pts',(2.61249699286393,-0.174890907412304,
1.94289029309402E-16));
#30899=CARTESIAN_POINT('Ctrl Pts',(2.59606370990205,-0.265394001643718,
2.67273655542046E-16));
#30900=CARTESIAN_POINT('Ctrl Pts',(2.57457910556097,-0.355167245076682,
-8.63540186836622E-17));
#30901=CARTESIAN_POINT('Ctrl Pts',(2.54820206281091,-0.443829678011398,
-1.94289029309402E-16));
#30902=CARTESIAN_POINT('Ctrl Pts',(2.5433159398537,-0.460253640057088,-2.14283072550056E-16));
#30903=CARTESIAN_POINT('Ctrl Pts',(2.53826078384047,-0.476642310793062,
2.54370247567095E-16));
#30904=CARTESIAN_POINT('Ctrl Pts',(2.53304532831965,-0.49296952041645,2.4980018054066E-16));
#30905=CARTESIAN_POINT('Ctrl Pts',(2.5060606614482,-0.577446189974434,2.26154741365496E-16));
#30906=CARTESIAN_POINT('Ctrl Pts',(2.47475215402615,-0.660408357948197,
3.47506847049484E-16));
#30907=CARTESIAN_POINT('Ctrl Pts',(2.43933604293942,-0.741555503604727,
2.77555756156289E-16));
#30908=CARTESIAN_POINT('Ctrl Pts',(2.40393876465244,-0.822659498618874,
2.07641862313994E-16));
#30909=CARTESIAN_POINT('Ctrl Pts',(2.3644375894048,-0.901951185787608,-1.23823437954767E-16));
#30910=CARTESIAN_POINT('Ctrl Pts',(2.32100582430644,-0.979100944080977,
-1.11022302462516E-16));
#30911=CARTESIAN_POINT('Ctrl Pts',(2.27823644108386,-1.05507408425856,-9.84163982743666E-17));
#30912=CARTESIAN_POINT('Ctrl Pts',(2.23165476456022,-1.1289707546069,2.53313632717541E-16));
#30913=CARTESIAN_POINT('Ctrl Pts',(2.18139506127574,-1.20043719637909,2.77555756156289E-16));
#30914=CARTESIAN_POINT('Ctrl Pts',(2.16608689289344,-1.2222045418435,2.84939454890925E-16));
#30915=CARTESIAN_POINT('Ctrl Pts',(2.15043733121093,-1.24374612322857,4.37114965090439E-17));
#30916=CARTESIAN_POINT('Ctrl Pts',(2.13444972694369,-1.26505107698559,0.));
#30917=CARTESIAN_POINT('Ctrl Pts',(2.12083931058568,-1.28318820912085,-3.72120586158607E-17));
#30918=CARTESIAN_POINT('Ctrl Pts',(2.10698390104784,-1.30115384375424,6.4814165885223E-17));
#30919=CARTESIAN_POINT('Ctrl Pts',(2.09288546869145,-1.31894102140198,5.55111512312578E-17));
#30920=CARTESIAN_POINT('Ctrl Pts',(2.08472665052523,-1.32923453095322,5.01274601200272E-17));
#30921=CARTESIAN_POINT('Ctrl Pts',(2.07648733901943,-1.33946704131009,1.07093663002969E-16));
#30922=CARTESIAN_POINT('Ctrl Pts',(2.06817568052718,-1.3496280615777,1.11022302462516E-16));
#30923=CARTESIAN_POINT('Ctrl Pts',(2.0141423836499,-1.41568388247163,1.36562011828508E-16));
#30924=CARTESIAN_POINT('Ctrl Pts',(1.95696807639868,-1.47883106712894,-2.06909962337776E-16));
#30925=CARTESIAN_POINT('Ctrl Pts',(1.89681447147471,-1.5387754276769,-2.22044604925031E-16));
#30926=CARTESIAN_POINT('Ctrl Pts',(1.83758356202805,-1.5978003023447,-2.36947097397864E-16));
#30927=CARTESIAN_POINT('Ctrl Pts',(1.77546340770889,-1.65372037608364,4.0590157288843E-16));
#30928=CARTESIAN_POINT('Ctrl Pts',(1.71058212140457,-1.70621256947127,4.44089209850063E-16));
#30929=CARTESIAN_POINT('Ctrl Pts',(1.64772546517897,-1.75706673624623,4.81085195985522E-16));
#30930=CARTESIAN_POINT('Ctrl Pts',(1.58227673616169,-1.80470390837557,2.58606592525932E-16));
#30931=CARTESIAN_POINT('Ctrl Pts',(1.5143365021986,-1.84878472647799,2.77555756156289E-16));
#30932=CARTESIAN_POINT('Ctrl Pts',(1.46963595841736,-1.87778722506477,2.90023153883192E-16));
#30933=CARTESIAN_POINT('Ctrl Pts',(1.42385657678108,-1.90524929950103,3.23574125955808E-17));
#30934=CARTESIAN_POINT('Ctrl Pts',(1.37702479013104,-1.93106208855763,5.55111512312578E-17));
#30935=CARTESIAN_POINT('Ctrl Pts',(0.261124777554701,2.92529416030267,11.058));
#30936=CARTESIAN_POINT('Ctrl Pts',(0.712806568001128,2.88599464153458,11.0335796606559));
#30937=CARTESIAN_POINT('Ctrl Pts',(1.15551467718148,2.74786827548953,11.0091593213117));
#30938=CARTESIAN_POINT('Ctrl Pts',(1.53904161881194,2.51335023952951,10.9847389819676));
#30939=CARTESIAN_POINT('Ctrl Pts',(2.36167356031087,2.01032944412425,10.9323594774631));
#30940=CARTESIAN_POINT('Ctrl Pts',(2.91203354584656,1.06384412118684,10.8799799729586));
#30941=CARTESIAN_POINT('Ctrl Pts',(2.94465829055491,0.100220893818898,10.8276004684541));
#30942=CARTESIAN_POINT('Ctrl Pts',(2.97728303526326,-0.863402333549067,
10.7752209639496));
#30943=CARTESIAN_POINT('Ctrl Pts',(2.49217253914424,-1.84416346534755,10.7228414594451));
#30944=CARTESIAN_POINT('Ctrl Pts',(1.70632723287924,-2.40227529678238,10.6704619549406));
#30945=CARTESIAN_POINT('Ctrl Pts',(0.92048192661426,-2.96038712821718,10.6180824504361));
#30946=CARTESIAN_POINT('Ctrl Pts',(-0.166098189796688,-3.09584965928835,
10.5657029459315));
#30947=CARTESIAN_POINT('Ctrl Pts',(-1.0650088521454,-2.74748941090806,10.513323441427));
#30948=CARTESIAN_POINT('Ctrl Pts',(-1.96391951449414,-2.39912916252775,
10.4609439369225));
#30949=CARTESIAN_POINT('Ctrl Pts',(-2.67516072278063,-1.56694613469595,
10.408564432418));
#30950=CARTESIAN_POINT('Ctrl Pts',(-2.87955920487239,-0.624834891848815,
10.3561849279135));
#30951=CARTESIAN_POINT('Ctrl Pts',(-2.92379628688831,-0.420937818389941,
10.3448486576389));
#30952=CARTESIAN_POINT('Ctrl Pts',(-2.94429281596354,-0.211891698741057,
10.3335123873642));
#30953=CARTESIAN_POINT('Ctrl Pts',(-2.94242444587263,-0.00248500551853048,
10.3221761170896));
#30954=CARTESIAN_POINT('Origin',(0.,0.,-1.84858989190501));
#30955=CARTESIAN_POINT('',(-1.37702479013099,-1.93106208855767,0.));
#30956=CARTESIAN_POINT('Ctrl Pts',(-1.37989654081094,-1.93326688769301,
3.07371315899641E-16));
#30957=CARTESIAN_POINT('Ctrl Pts',(-0.801986922861967,-2.34019513141193,
0.0475906520026623));
#30958=CARTESIAN_POINT('Ctrl Pts',(0.824868299691477,-2.62988338064349,
0.147626409229032));
#30959=CARTESIAN_POINT('Ctrl Pts',(2.66596861578497,-0.838738147770652,
0.30010727167911));
#30960=CARTESIAN_POINT('Ctrl Pts',(2.16631806184957,1.76615982799916,0.457442587350233));
#30961=CARTESIAN_POINT('Ctrl Pts',(-0.283824062622952,2.78024166545816,
0.614777903021357));
#30962=CARTESIAN_POINT('Ctrl Pts',(-2.10236314538525,1.54689613835291,0.745160337872953));
#30963=CARTESIAN_POINT('Ctrl Pts',(-2.3682722008076,0.381486792202907,0.823097667500842));
#30964=CARTESIAN_POINT('Ctrl Pts',(-2.36802324146013,0.000186122305323062,
0.848589891905023));
#30965=CARTESIAN_POINT('Origin',(0.,0.,0.));
#30966=CARTESIAN_POINT('Ctrl Pts',(-1.03908919352509,2.13201587949044,-0.329233991005384));
#30967=CARTESIAN_POINT('Ctrl Pts',(-1.74163600084562,1.78961280339009,-0.276788885781676));
#30968=CARTESIAN_POINT('Ctrl Pts',(-2.77044124913769,0.362429281341372,
-0.171898675334261));
#30969=CARTESIAN_POINT('Ctrl Pts',(-1.82442757362648,-2.1194917921021,-0.0145633596631371));
#30970=CARTESIAN_POINT('Ctrl Pts',(0.766254154833431,-2.68690713172521,
0.142771956007986));
#30971=CARTESIAN_POINT('Ctrl Pts',(2.66596861578497,-0.838738147770652,
0.30010727167911));
#30972=CARTESIAN_POINT('Ctrl Pts',(2.16631806184957,1.76615982799916,0.457442587350233));
#30973=CARTESIAN_POINT('Ctrl Pts',(-0.283824062622952,2.78024166545816,
0.614777903021357));
#30974=CARTESIAN_POINT('Ctrl Pts',(-2.47829466728951,1.29193683314281,0.772113218692479));
#30975=CARTESIAN_POINT('Ctrl Pts',(-2.44182858239548,-1.35964121596809,
0.929448534363604));
#30976=CARTESIAN_POINT('Ctrl Pts',(-0.207121339063888,-2.78711087979173,
1.08678385003473));
#30977=CARTESIAN_POINT('Ctrl Pts',(2.21401803077907,-1.70561830406782,1.24411916570585));
#30978=CARTESIAN_POINT('Ctrl Pts',(2.64205485235054,0.911349150745493,1.40145448137697));
#30979=CARTESIAN_POINT('Ctrl Pts',(0.691640660298454,2.70787919402874,1.5587897970481));
#30980=CARTESIAN_POINT('Ctrl Pts',(-1.88140253096646,2.06671733364312,1.71612511271922));
#30981=CARTESIAN_POINT('Ctrl Pts',(-2.76076141176456,-0.43496057134077,
1.87346042839035));
#30982=CARTESIAN_POINT('Ctrl Pts',(-1.15481219883121,-2.54507342378116,
2.03079574406147));
#30983=CARTESIAN_POINT('Ctrl Pts',(1.49072764255621,-2.36404822464922,2.18813105973259));
#30984=CARTESIAN_POINT('Ctrl Pts',(2.79427705549031,-0.0548463935276453,
2.34546637540372));
#30985=CARTESIAN_POINT('Ctrl Pts',(1.5823475414007,2.30372918060613,2.50280169107483));
#30986=CARTESIAN_POINT('Ctrl Pts',(-1.05405113312049,2.58842974112365,2.66013700674597));
#30987=CARTESIAN_POINT('Ctrl Pts',(-2.74156638658485,0.542960359863138,
2.81747232241708));
#30988=CARTESIAN_POINT('Ctrl Pts',(-1.9610543025963,-1.99129560121778,2.97480763808821));
#30989=CARTESIAN_POINT('Ctrl Pts',(0.584848394656438,-2.73293698550247,
3.13214295375933));
#30990=CARTESIAN_POINT('Ctrl Pts',(2.60425579784155,-1.01431944186932,3.28947826943046));
#30991=CARTESIAN_POINT('Ctrl Pts',(2.27924634057658,1.61741407950708,3.44681358510158));
#30992=CARTESIAN_POINT('Ctrl Pts',(-0.0975982492034651,2.79311059143494,
3.6041489007727));
#30993=CARTESIAN_POINT('Ctrl Pts',(-2.38658243027454,1.45437838755459,3.76148421644382));
#30994=CARTESIAN_POINT('Ctrl Pts',(-2.52710481755741,-1.19362198012869,
3.91881953211495));
#30995=CARTESIAN_POINT('Ctrl Pts',(-0.392663608746353,-2.76709368867159,
4.07615484778607));
#30996=CARTESIAN_POINT('Ctrl Pts',(2.09526330020315,-1.8495577562663,4.23349016345719));
#30997=CARTESIAN_POINT('Ctrl Pts',(2.69698125586998,0.732996791565816,4.39082547912832));
#30998=CARTESIAN_POINT('Ctrl Pts',(0.870808554093777,2.65568911080063,4.54816079479944));
#30999=CARTESIAN_POINT('Ctrl Pts',(-1.73928800639316,2.18766300463189,4.70549611047057));
#31000=CARTESIAN_POINT('Ctrl Pts',(-2.78363356575401,-0.249752602863106,
4.86283142614169));
#31001=CARTESIAN_POINT('Ctrl Pts',(-1.32208186928512,-2.46233460804071,
5.02016674181281));
#31002=CARTESIAN_POINT('Ctrl Pts',(1.32964132424929,-2.45826079574207,5.17750205748394));
#31003=CARTESIAN_POINT('Ctrl Pts',(2.78438780839412,-0.241198514719961,
5.33483737315506));
#31004=CARTESIAN_POINT('Ctrl Pts',(1.73255804842731,2.19299676239354,5.49217268882618));
#31005=CARTESIAN_POINT('Ctrl Pts',(-0.878964234485193,2.65300095467984,
5.64950800449731));
#31006=CARTESIAN_POINT('Ctrl Pts',(-2.69922070918587,0.72470666765315,5.80684332016843));
#31007=CARTESIAN_POINT('Ctrl Pts',(-2.08957051396587,-1.85598686908106,
5.96417863583956));
#31008=CARTESIAN_POINT('Ctrl Pts',(0.401163844498212,-2.76587414046649,
6.12151395151068));
#31009=CARTESIAN_POINT('Ctrl Pts',(2.53076037597685,-1.18585163930103,6.2788492671818));
#31010=CARTESIAN_POINT('Ctrl Pts',(2.38210248511723,1.46170446446183,6.43618458285292));
#31011=CARTESIAN_POINT('Ctrl Pts',(0.0890157606711408,2.793397283841,6.59351989852405));
#31012=CARTESIAN_POINT('Ctrl Pts',(-2.28420520026003,1.61040330172691,6.75085521419516));
#31013=CARTESIAN_POINT('Ctrl Pts',(-2.60112693645964,-1.02231641451357,
6.9081905298663));
#31014=CARTESIAN_POINT('Ctrl Pts',(-0.57644849505612,-2.73472106868152,
7.06552584553741));
#31015=CARTESIAN_POINT('Ctrl Pts',(1.96716344393165,-1.98526073259378,7.22286116120855));
#31016=CARTESIAN_POINT('Ctrl Pts',(2.73988515609665,0.551381466653972,7.38019647687966));
#31017=CARTESIAN_POINT('Ctrl Pts',(1.04609303646807,2.5916561403346,7.53753179255079));
#31018=CARTESIAN_POINT('Ctrl Pts',(-1.58941846186445,2.2988564868904,7.69486710822191));
#31019=CARTESIAN_POINT('Ctrl Pts',(-2.79409530723714,-0.0634318507917163,
7.85220242389303));
#31020=CARTESIAN_POINT('Ctrl Pts',(-1.48345697628832,-2.36861723168749,
8.00953773956416));
#31021=CARTESIAN_POINT('Ctrl Pts',(1.16262680634646,-2.54151354917186,8.16687305523529));
#31022=CARTESIAN_POINT('Ctrl Pts',(2.76208455499713,-0.426475157784177,
8.3242083709064));
#31023=CARTESIAN_POINT('Ctrl Pts',(1.8750440359881,2.07248692819523,8.48154368657753));
#31024=CARTESIAN_POINT('Ctrl Pts',(-0.699958537943023,2.7057439570526,8.63887900224866));
#31025=CARTESIAN_POINT('Ctrl Pts',(-2.6448406647993,0.903221864868725,8.79621431791976));
#31026=CARTESIAN_POINT('Ctrl Pts',(-2.20877058145475,-1.7124032551425,8.95354963359091));
#31027=CARTESIAN_POINT('Ctrl Pts',(0.215690902196592,-2.78647992051942,
9.11088494926201));
#31028=CARTESIAN_POINT('Ctrl Pts',(2.4459813653409,-1.35209655994371,9.26822026493315));
#31029=CARTESIAN_POINT('Ctrl Pts',(2.47433880171217,1.29947749716991,9.42555558060427));
#31030=CARTESIAN_POINT('Ctrl Pts',(0.275231669725872,2.78123058171878,9.58289089627539));
#31031=CARTESIAN_POINT('Ctrl Pts',(-2.17164161907558,1.7592467736877,9.74022621194653));
#31032=CARTESIAN_POINT('Ctrl Pts',(-2.66355657074516,-0.846449946443288,
9.89756152761763));
#31033=CARTESIAN_POINT('Ctrl Pts',(-0.757654725048104,-2.69016151139635,
10.0548968432888));
#31034=CARTESIAN_POINT('Ctrl Pts',(1.83027666927001,-2.11210170665972,10.2122321589599));
#31035=CARTESIAN_POINT('Ctrl Pts',(2.77060484795253,0.367287133540841,10.369567474631));
#31036=CARTESIAN_POINT('Ctrl Pts',(1.21665350181368,2.51610800548609,10.5269027903021));
#31037=CARTESIAN_POINT('Ctrl Pts',(-1.43234772356642,2.39972494583597,10.6842381059733));
#31038=CARTESIAN_POINT('Ctrl Pts',(-2.79231938150401,0.123316482315984,
10.8415734216444));
#31039=CARTESIAN_POINT('Ctrl Pts',(-1.63779792657952,-2.26461658842463,
10.9989087373155));
#31040=CARTESIAN_POINT('Ctrl Pts',(0.989622905930635,-2.61290295808564,
11.1562440529866));
#31041=CARTESIAN_POINT('Ctrl Pts',(2.72902843688469,-0.61088887604173,11.3135793686578));
#31042=CARTESIAN_POINT('Ctrl Pts',(2.00599839187704,1.9449087769569,11.4709146843289));
#31043=CARTESIAN_POINT('Ctrl Pts',(0.328567026486064,2.47549058867235,11.5758048947763));
#31044=CARTESIAN_POINT('Ctrl Pts',(-0.439445221994061,2.3306835819919,11.62825));
#31045=CARTESIAN_POINT('Ctrl Pts',(-1.12236674703447,2.30288577939268,-0.219489327336923));
#31046=CARTESIAN_POINT('Ctrl Pts',(-1.881218999262,1.93304089110777,-0.167044222113215));
#31047=CARTESIAN_POINT('Ctrl Pts',(-2.9924775967461,0.391476088928602,-0.0621540116657994));
#31048=CARTESIAN_POINT('Ctrl Pts',(-1.97064588273166,-2.28935795203269,
0.0951813040053245));
#31049=CARTESIAN_POINT('Ctrl Pts',(0.82766540978493,-2.90224865758394,0.252516619676447));
#31050=CARTESIAN_POINT('Ctrl Pts',(2.87963202931947,-0.905958614903406,
0.409851935347572));
#31051=CARTESIAN_POINT('Ctrl Pts',(2.33993710190716,1.90770828264466,0.567187251018694));
#31052=CARTESIAN_POINT('Ctrl Pts',(-0.306571073860874,3.00306346507554,
0.724522566689817));
#31053=CARTESIAN_POINT('Ctrl Pts',(-2.67691699735827,1.39547879991837,0.881857882360941));
#31054=CARTESIAN_POINT('Ctrl Pts',(-2.63752834686069,-1.46860933422193,
1.03919319803207));
#31055=CARTESIAN_POINT('Ctrl Pts',(-0.223721028969555,-3.01048321093979,
1.19652851370319));
#31056=CARTESIAN_POINT('Ctrl Pts',(2.39145997337443,-1.84231467283839,1.35386382937431));
#31057=CARTESIAN_POINT('Ctrl Pts',(2.85380170306596,0.984389009248359,1.51119914504543));
#31058=CARTESIAN_POINT('Ctrl Pts',(0.747072034675363,2.92490152077689,1.66853446071656));
#31059=CARTESIAN_POINT('Ctrl Pts',(-2.03218708432488,2.23235389729304,1.82586977638768));
#31060=CARTESIAN_POINT('Ctrl Pts',(-2.98202197113476,-0.469820381720866,
1.98320509205881));
#31061=CARTESIAN_POINT('Ctrl Pts',(-1.24736434476896,-2.74904772122835,
2.14054040772993));
#31062=CARTESIAN_POINT('Ctrl Pts',(1.61020165094208,-2.55351430104939,2.29787572340105));
#31063=CARTESIAN_POINT('Ctrl Pts',(3.01822371806624,-0.0592420445461263,
2.45521103907218));
#31064=CARTESIAN_POINT('Ctrl Pts',(1.70916440454448,2.48836100172844,2.6125463547433));
#31065=CARTESIAN_POINT('Ctrl Pts',(-1.13852780768032,2.79587882019688,2.76988167041443));
#31066=CARTESIAN_POINT('Ctrl Pts',(-2.9612885652785,0.586475787319947,2.92721698608554));
#31067=CARTESIAN_POINT('Ctrl Pts',(-2.11822252803541,-2.15088750826171,
3.08455230175667));
#31068=CARTESIAN_POINT('Ctrl Pts',(0.631720928587459,-2.95196756292179,
3.24188761742779));
#31069=CARTESIAN_POINT('Ctrl Pts',(2.81297325242419,-1.09561182958951,3.39922293309892));
#31070=CARTESIAN_POINT('Ctrl Pts',(2.46191599037299,1.74704134191371,3.55655824877004));
#31071=CARTESIAN_POINT('Ctrl Pts',(-0.105420237413036,3.01696376802969,
3.71389356444116));
#31072=CARTESIAN_POINT('Ctrl Pts',(-2.57785450516496,1.57093919364055,3.87122888011228));
#31073=CARTESIAN_POINT('Ctrl Pts',(-2.72963902538035,-1.28928452665457,
4.02856419578341));
#31074=CARTESIAN_POINT('Ctrl Pts',(-0.424133539231963,-2.98886174685155,
4.18589951145453));
#31075=CARTESIAN_POINT('Ctrl Pts',(2.26318767347756,-1.99779011781522,4.34323482712566));
#31076=CARTESIAN_POINT('Ctrl Pts',(2.91313016998542,0.791742643136777,4.50057014279678));
#31077=CARTESIAN_POINT('Ctrl Pts',(0.940599296228219,2.86852867588043,4.6579054584679));
#31078=CARTESIAN_POINT('Ctrl Pts',(-1.87868282535885,2.36299272999521,4.81524077413902));
#31079=CARTESIAN_POINT('Ctrl Pts',(-3.00672720840483,-0.269768965152914,
4.97257608981016));
#31080=CARTESIAN_POINT('Ctrl Pts',(-1.42803980273229,-2.65967782299944,
5.12991140548127));
#31081=CARTESIAN_POINT('Ctrl Pts',(1.43620510839645,-2.65527751599392,5.28724672115241));
#31082=CARTESIAN_POINT('Ctrl Pts',(3.00754189963992,-0.260529311672868,
5.44458203682351));
#31083=CARTESIAN_POINT('Ctrl Pts',(1.87141349653044,2.36875396048986,5.60191735249465));
#31084=CARTESIAN_POINT('Ctrl Pts',(-0.949408611663097,2.86562507813386,
5.75925266816576));
#31085=CARTESIAN_POINT('Ctrl Pts',(-2.9155491037487,0.782788109236974,5.9165879838369));
#31086=CARTESIAN_POINT('Ctrl Pts',(-2.25703864025646,-2.00473449033026,
6.07392329950801));
#31087=CARTESIAN_POINT('Ctrl Pts',(0.433315024333776,-2.98754445824887,
6.23125861517914));
#31088=CARTESIAN_POINT('Ctrl Pts',(2.73358755765012,-1.28089143373012,6.38859393085026));
#31089=CARTESIAN_POINT('Ctrl Pts',(2.57301551588047,1.57885241721953,6.54592924652138));
#31090=CARTESIAN_POINT('Ctrl Pts',(0.0961499074014511,3.01727343732968,
6.70326456219251));
#31091=CARTESIAN_POINT('Ctrl Pts',(-2.46727227667312,1.73946868703451,6.86059987786364));
#31092=CARTESIAN_POINT('Ctrl Pts',(-2.80959362919934,-1.104249717683,7.01793519353475));
#31093=CARTESIAN_POINT('Ctrl Pts',(-0.622647821053927,-2.95389463101813,
7.17527050920589));
#31094=CARTESIAN_POINT('Ctrl Pts',(2.12482128503379,-2.14436897654329,7.33260582487699));
#31095=CARTESIAN_POINT('Ctrl Pts',(2.95947259297716,0.59557180168919,7.48994114054813));
#31096=CARTESIAN_POINT('Ctrl Pts',(1.12993191128569,2.79936379839662,7.64727645621924));
#31097=CARTESIAN_POINT('Ctrl Pts',(-1.71680202222819,2.4830977871468,7.80461177189038));
#31098=CARTESIAN_POINT('Ctrl Pts',(-3.01802740364303,-0.0685155812177535,
7.96194708756148));
#31099=CARTESIAN_POINT('Ctrl Pts',(-1.60234827887482,-2.55844949005786,
8.11928240323263));
#31100=CARTESIAN_POINT('Ctrl Pts',(1.25580525212405,-2.74520254132467,8.27661771890373));
#31101=CARTESIAN_POINT('Ctrl Pts',(2.98345115736347,-0.460654906735591,
8.43395303457487));
#31102=CARTESIAN_POINT('Ctrl Pts',(2.02531898929576,2.23858589461288,8.591288350246));
#31103=CARTESIAN_POINT('Ctrl Pts',(-0.756056546623237,2.92259515574686,
8.74862366591711));
#31104=CARTESIAN_POINT('Ctrl Pts',(-2.85681078378342,0.975610363999675,
8.90595898158824));
#31105=CARTESIAN_POINT('Ctrl Pts',(-2.38579196848608,-1.84964340218511,
9.06329429725935));
#31106=CARTESIAN_POINT('Ctrl Pts',(0.232977397678477,-3.00980168358836,
9.2206296129305));
#31107=CARTESIAN_POINT('Ctrl Pts',(2.6420139535965,-1.46046001355504,9.37796492860159));
#31108=CARTESIAN_POINT('Ctrl Pts',(2.67264408988566,1.40362380865033,9.53530024427275));
#31109=CARTESIAN_POINT('Ctrl Pts',(0.297290045701602,3.00413163779202,9.69263555994384));
#31110=CARTESIAN_POINT('Ctrl Pts',(-2.34568731434669,1.90024118325806,9.84997087561499));
#31111=CARTESIAN_POINT('Ctrl Pts',(-2.87702667151006,-0.914288473825907,
10.0073061912861));
#31112=CARTESIAN_POINT('Ctrl Pts',(-0.818376780767691,-2.90576385873112,
10.1646415069572));
#31113=CARTESIAN_POINT('Ctrl Pts',(1.97696375273877,-2.2813755899699,10.3219768226283));
#31114=CARTESIAN_POINT('Ctrl Pts',(2.99265430714862,0.396723272524227,10.4793121382995));
#31115=CARTESIAN_POINT('Ctrl Pts',(1.31416190410585,2.71776087645035,10.6366474539706));
#31116=CARTESIAN_POINT('Ctrl Pts',(-1.54714288738549,2.59205032447523,10.7939827696417));
#31117=CARTESIAN_POINT('Ctrl Pts',(-3.01610914676913,0.133199652133039,
10.9513180853128));
#31118=CARTESIAN_POINT('Ctrl Pts',(-1.76905884750739,-2.44611374025332,
11.108653400984));
#31119=CARTESIAN_POINT('Ctrl Pts',(1.06893599571762,-2.82231343724637,11.2659887166551));
#31120=CARTESIAN_POINT('Ctrl Pts',(2.94774576461505,-0.659848418090555,
11.4233240323262));
#31121=CARTESIAN_POINT('Ctrl Pts',(2.1667686505423,2.10078302312668,11.5806593479973));
#31122=CARTESIAN_POINT('Ctrl Pts',(0.35489995180194,2.67388818653474,11.6855495584447));
#31123=CARTESIAN_POINT('Ctrl Pts',(-0.474664453622185,2.51747565713064,
11.7379946636685));
#31124=CARTESIAN_POINT('Ctrl Pts',(-1.20564430054384,2.47375567929493,-0.109744663668461));
#31125=CARTESIAN_POINT('Ctrl Pts',(-2.02080199767838,2.07646897882546,-0.0572995584447534));
#31126=CARTESIAN_POINT('Ctrl Pts',(-3.21451394435451,0.420522896515832,
0.0475906520026618));
#31127=CARTESIAN_POINT('Ctrl Pts',(-2.11686419183683,-2.45922411196328,
0.204925967673786));
#31128=CARTESIAN_POINT('Ctrl Pts',(0.88907666473643,-3.11759018344267,0.362261283344908));
#31129=CARTESIAN_POINT('Ctrl Pts',(3.09329544285396,-0.973179082036162,
0.519596599016033));
#31130=CARTESIAN_POINT('Ctrl Pts',(2.51355614196476,2.04925673729017,0.676931914687155));
#31131=CARTESIAN_POINT('Ctrl Pts',(-0.329318085098797,3.22588526469291,
0.83426723035828));
#31132=CARTESIAN_POINT('Ctrl Pts',(-2.87553932742704,1.49902076669393,0.991602546029402));
#31133=CARTESIAN_POINT('Ctrl Pts',(-2.8332281113259,-1.57757745247578,1.14893786170053));
#31134=CARTESIAN_POINT('Ctrl Pts',(-0.240320718875223,-3.23385554208785,
1.30627317737165));
#31135=CARTESIAN_POINT('Ctrl Pts',(2.5689019159698,-1.97901104160895,1.46360849304277));
#31136=CARTESIAN_POINT('Ctrl Pts',(3.06554855378139,1.05742886775122,1.6209438087139));
#31137=CARTESIAN_POINT('Ctrl Pts',(0.802503409052275,3.14192384752506,1.77827912438502));
#31138=CARTESIAN_POINT('Ctrl Pts',(-2.18297163768331,2.39799046094296,1.93561444005614));
#31139=CARTESIAN_POINT('Ctrl Pts',(-3.20328253050495,-0.504680192100957,
2.09294975572727));
#31140=CARTESIAN_POINT('Ctrl Pts',(-1.33991649070671,-2.95302201867555,
2.25028507139839));
#31141=CARTESIAN_POINT('Ctrl Pts',(1.72967565932795,-2.74298037744955,2.40762038706951));
#31142=CARTESIAN_POINT('Ctrl Pts',(3.24217038064216,-0.0636376955646108,
2.56495570274064));
#31143=CARTESIAN_POINT('Ctrl Pts',(1.83598126768827,2.67299282285076,2.72229101841176));
#31144=CARTESIAN_POINT('Ctrl Pts',(-1.22300448224015,3.00332789927011,2.87962633408289));
#31145=CARTESIAN_POINT('Ctrl Pts',(-3.18101074397215,0.629991214776759,
3.036961649754));
#31146=CARTESIAN_POINT('Ctrl Pts',(-2.27539075347452,-2.31047941530565,
3.19429696542514));
#31147=CARTESIAN_POINT('Ctrl Pts',(0.678593462518484,-3.1709981403411,3.35163228109625));
#31148=CARTESIAN_POINT('Ctrl Pts',(3.02169070700682,-1.1769042173097,3.50896759676738));
#31149=CARTESIAN_POINT('Ctrl Pts',(2.64458564016939,1.87666860432035,3.6663029124385));
#31150=CARTESIAN_POINT('Ctrl Pts',(-0.113242225622608,3.24081694462443,
3.82363822810962));
#31151=CARTESIAN_POINT('Ctrl Pts',(-2.76912658005537,1.68749999972651,3.98097354378075));
#31152=CARTESIAN_POINT('Ctrl Pts',(-2.93217323320329,-1.38494707318046,
4.13830885945187));
#31153=CARTESIAN_POINT('Ctrl Pts',(-0.45560346971757,-3.21062980503151,
4.295644175123));
#31154=CARTESIAN_POINT('Ctrl Pts',(2.43111204675198,-2.14602247936414,4.45297949079412));
#31155=CARTESIAN_POINT('Ctrl Pts',(3.12927908410086,0.850488494707743,4.61031480646524));
#31156=CARTESIAN_POINT('Ctrl Pts',(1.01039003836266,3.08136824096022,4.76765012213636));
#31157=CARTESIAN_POINT('Ctrl Pts',(-2.01807764432454,2.53832245535854,4.92498543780749));
#31158=CARTESIAN_POINT('Ctrl Pts',(-3.22982085105565,-0.289785327442726,
5.08232075347861));
#31159=CARTESIAN_POINT('Ctrl Pts',(-1.53399773617946,-2.85702103795818,
5.23965606914974));
#31160=CARTESIAN_POINT('Ctrl Pts',(1.5427688925436,-2.85229423624577,5.39699138482085));
#31161=CARTESIAN_POINT('Ctrl Pts',(3.23069599088573,-0.279860108625777,
5.55432670049199));
#31162=CARTESIAN_POINT('Ctrl Pts',(2.01026894463356,2.54451115858618,5.7116620161631));
#31163=CARTESIAN_POINT('Ctrl Pts',(-1.019852988841,3.07824920158788,5.86899733183423));
#31164=CARTESIAN_POINT('Ctrl Pts',(-3.13187749831153,0.840869550820803,
6.02633264750535));
#31165=CARTESIAN_POINT('Ctrl Pts',(-2.42450676654705,-2.15348211157947,
6.18366796317648));
#31166=CARTESIAN_POINT('Ctrl Pts',(0.465466204169338,-3.20921477603124,
6.3410032788476));
#31167=CARTESIAN_POINT('Ctrl Pts',(2.93641473932339,-1.3759312281592,6.49833859451872));
#31168=CARTESIAN_POINT('Ctrl Pts',(2.76392854664371,1.69600036997724,6.65567391018985));
#31169=CARTESIAN_POINT('Ctrl Pts',(0.103284054131762,3.24114959081836,6.81300922586097));
#31170=CARTESIAN_POINT('Ctrl Pts',(-2.65033935308621,1.86853407234211,6.97034454153209));
#31171=CARTESIAN_POINT('Ctrl Pts',(-3.01806032193904,-1.18618302085242,
7.12767985720322));
#31172=CARTESIAN_POINT('Ctrl Pts',(-0.668847147051728,-3.17306819335475,
7.28501517287434));
#31173=CARTESIAN_POINT('Ctrl Pts',(2.28247912613591,-2.30347722049279,7.44235048854546));
#31174=CARTESIAN_POINT('Ctrl Pts',(3.17906002985769,0.639762136724403,7.59968580421659));
#31175=CARTESIAN_POINT('Ctrl Pts',(1.2137707861033,3.00707145645863,7.75702111988771));
#31176=CARTESIAN_POINT('Ctrl Pts',(-1.84418558259193,2.66733908740319,7.91435643555884));
#31177=CARTESIAN_POINT('Ctrl Pts',(-3.24195950004891,-0.0735993116437874,
8.07169175122995));
#31178=CARTESIAN_POINT('Ctrl Pts',(-1.7212395814613,-2.74828174842822,8.22902706690109));
#31179=CARTESIAN_POINT('Ctrl Pts',(1.34898369790163,-2.94889153347749,8.38636238257219));
#31180=CARTESIAN_POINT('Ctrl Pts',(3.20481775972981,-0.494834655687006,
8.54369769824334));
#31181=CARTESIAN_POINT('Ctrl Pts',(2.17559394260342,2.40468486103055,8.70103301391445));
#31182=CARTESIAN_POINT('Ctrl Pts',(-0.812154555303452,3.13944635444111,
8.85836832958556));
#31183=CARTESIAN_POINT('Ctrl Pts',(-3.06878090276754,1.04799886313063,9.01570364525671));
#31184=CARTESIAN_POINT('Ctrl Pts',(-2.56281335551741,-1.98688354922771,
9.17303896092782));
#31185=CARTESIAN_POINT('Ctrl Pts',(0.250263893160364,-3.23312344665729,
9.33037427659894));
#31186=CARTESIAN_POINT('Ctrl Pts',(2.83804654185209,-1.56882346716636,9.48770959227006));
#31187=CARTESIAN_POINT('Ctrl Pts',(2.87094937805915,1.50777012013074,9.64504490794121));
#31188=CARTESIAN_POINT('Ctrl Pts',(0.31934842167733,3.22703269386527,9.8023802236123));
#31189=CARTESIAN_POINT('Ctrl Pts',(-2.5197330096178,2.04123559282842,9.95971553928346));
#31190=CARTESIAN_POINT('Ctrl Pts',(-3.09049677227496,-0.982127001208522,
10.1170508549545));
#31191=CARTESIAN_POINT('Ctrl Pts',(-0.879098836487281,-3.1213662060659,
10.2743861706257));
#31192=CARTESIAN_POINT('Ctrl Pts',(2.12365083620754,-2.45064947328008,10.4317214862968));
#31193=CARTESIAN_POINT('Ctrl Pts',(3.2147037663447,0.426159411507612,10.5890568019679));
#31194=CARTESIAN_POINT('Ctrl Pts',(1.41167030639802,2.9194137474146,10.7463921176391));
#31195=CARTESIAN_POINT('Ctrl Pts',(-1.66193805120456,2.78437570311449,10.9037274333102));
#31196=CARTESIAN_POINT('Ctrl Pts',(-3.23989891203425,0.143082821950096,
11.0610627489813));
#31197=CARTESIAN_POINT('Ctrl Pts',(-1.90031976843527,-2.627610892082,11.2183980646524));
#31198=CARTESIAN_POINT('Ctrl Pts',(1.1482490855046,-3.0317239164071,11.3757333803236));
#31199=CARTESIAN_POINT('Ctrl Pts',(3.16646309234541,-0.708807960139384,
11.5330686959947));
#31200=CARTESIAN_POINT('Ctrl Pts',(2.32753890920755,2.25665726929647,11.6904040116658));
#31201=CARTESIAN_POINT('Ctrl Pts',(0.381232877117816,2.87228578439713,11.7952942221132));
#31202=CARTESIAN_POINT('Ctrl Pts',(-0.50988368525031,2.70426773226937,11.8477393273369));
#31203=CARTESIAN_POINT('Ctrl Pts',(-1.28892185405322,2.64462557919718,0.));
#31204=CARTESIAN_POINT('Ctrl Pts',(-2.16038499609476,2.21989706654315,0.0524451052237078));
#31205=CARTESIAN_POINT('Ctrl Pts',(-3.43655029196293,0.449569704103062,
0.157335315671123));
#31206=CARTESIAN_POINT('Ctrl Pts',(-2.26308250094201,-2.62909027189387,
0.314670631342247));
#31207=CARTESIAN_POINT('Ctrl Pts',(0.950487919687924,-3.33293170930141,
0.47200594701337));
#31208=CARTESIAN_POINT('Ctrl Pts',(3.30695885638846,-1.04039954916892,0.629341262684495));
#31209=CARTESIAN_POINT('Ctrl Pts',(2.68717518202235,2.19080519193567,0.786676578355616));
#31210=CARTESIAN_POINT('Ctrl Pts',(-0.352065096336719,3.44870706431028,
0.944011894026741));
#31211=CARTESIAN_POINT('Ctrl Pts',(-3.0741616574958,1.60256273346949,1.10134720969786));
#31212=CARTESIAN_POINT('Ctrl Pts',(-3.02892787579111,-1.68654557072963,
1.25868252536899));
#31213=CARTESIAN_POINT('Ctrl Pts',(-0.256920408780888,-3.45722787323591,
1.41601784104011));
#31214=CARTESIAN_POINT('Ctrl Pts',(2.74634385856517,-2.11570741037952,1.57335315671124));
#31215=CARTESIAN_POINT('Ctrl Pts',(3.27729540449682,1.13046872625408,1.73068847238236));
#31216=CARTESIAN_POINT('Ctrl Pts',(0.857934783429182,3.35894617427322,1.88802378805348));
#31217=CARTESIAN_POINT('Ctrl Pts',(-2.33375619104173,2.56362702459287,2.0453591037246));
#31218=CARTESIAN_POINT('Ctrl Pts',(-3.42454308987515,-0.539540002481048,
2.20269441939573));
#31219=CARTESIAN_POINT('Ctrl Pts',(-1.43246863664446,-3.15699631612275,
2.36002973506685));
#31220=CARTESIAN_POINT('Ctrl Pts',(1.84914966771382,-2.93244645384971,2.51736505073797));
#31221=CARTESIAN_POINT('Ctrl Pts',(3.46611704321809,-0.0680333465830936,
2.6747003664091));
#31222=CARTESIAN_POINT('Ctrl Pts',(1.96279813083206,2.85762464397308,2.83203568208022));
#31223=CARTESIAN_POINT('Ctrl Pts',(-1.30748115679998,3.21077697834334,2.98937099775135));
#31224=CARTESIAN_POINT('Ctrl Pts',(-3.40073292266579,0.673506642233569,
3.14670631342246));
#31225=CARTESIAN_POINT('Ctrl Pts',(-2.43255897891363,-2.47007132234958,
3.3040416290936));
#31226=CARTESIAN_POINT('Ctrl Pts',(0.725465996449509,-3.39002871776042,
3.46137694476471));
#31227=CARTESIAN_POINT('Ctrl Pts',(3.23040816158946,-1.2581966050299,3.61871226043584));
#31228=CARTESIAN_POINT('Ctrl Pts',(2.8272552899658,2.00629586672699,3.77604757610696));
#31229=CARTESIAN_POINT('Ctrl Pts',(-0.12106421383218,3.46467012121918,3.93338289177809));
#31230=CARTESIAN_POINT('Ctrl Pts',(-2.96039865494578,1.80406080581246,4.09071820744921));
#31231=CARTESIAN_POINT('Ctrl Pts',(-3.13470744102623,-1.48060961970634,
4.24805352312033));
#31232=CARTESIAN_POINT('Ctrl Pts',(-0.48707340020318,-3.43239786321147,
4.40538883879146));
#31233=CARTESIAN_POINT('Ctrl Pts',(2.59903642002639,-2.29425484091306,4.56272415446258));
#31234=CARTESIAN_POINT('Ctrl Pts',(3.3454279982163,0.909234346278705,4.7200594701337));
#31235=CARTESIAN_POINT('Ctrl Pts',(1.0801807804971,3.29420780604002,4.87739478580482));
#31236=CARTESIAN_POINT('Ctrl Pts',(-2.15747246329023,2.71365218072187,5.03473010147595));
#31237=CARTESIAN_POINT('Ctrl Pts',(-3.45291449370647,-0.309801689732533,
5.19206541714708));
#31238=CARTESIAN_POINT('Ctrl Pts',(-1.63995566962662,-3.05436425291692,
5.34940073281819));
#31239=CARTESIAN_POINT('Ctrl Pts',(1.64933267669075,-3.04931095649762,5.50673604848933));
#31240=CARTESIAN_POINT('Ctrl Pts',(3.45385008213154,-0.299190905578683,
5.66407136416044));
#31241=CARTESIAN_POINT('Ctrl Pts',(2.14912439273668,2.7202683566825,5.82140667983157));
#31242=CARTESIAN_POINT('Ctrl Pts',(-1.0902973660189,3.2908733250419,5.97874199550268));
#31243=CARTESIAN_POINT('Ctrl Pts',(-3.34820589287437,0.898950992404627,
6.13607731117382));
#31244=CARTESIAN_POINT('Ctrl Pts',(-2.59197489283764,-2.30222973282867,
6.29341262684493));
#31245=CARTESIAN_POINT('Ctrl Pts',(0.497617384004899,-3.43088509381362,
6.45074794251607));
#31246=CARTESIAN_POINT('Ctrl Pts',(3.13924192099666,-1.47097102258828,6.60808325818718));
#31247=CARTESIAN_POINT('Ctrl Pts',(2.95484157740695,1.81314832273494,6.76541857385831));
#31248=CARTESIAN_POINT('Ctrl Pts',(0.110418200862072,3.46502574430704,6.92275388952943));
#31249=CARTESIAN_POINT('Ctrl Pts',(-2.8334064294993,1.9975994576497,7.08008920520056));
#31250=CARTESIAN_POINT('Ctrl Pts',(-3.22652701467874,-1.26811632402185,
7.23742452087168));
#31251=CARTESIAN_POINT('Ctrl Pts',(-0.715046473049532,-3.39224175569136,
7.3947598365428));
#31252=CARTESIAN_POINT('Ctrl Pts',(2.44013696723805,-2.46258546444229,7.55209515221393));
#31253=CARTESIAN_POINT('Ctrl Pts',(3.39864746673821,0.683952471759619,7.70943046788505));
#31254=CARTESIAN_POINT('Ctrl Pts',(1.29760966092091,3.21477911452065,7.86676578355617));
#31255=CARTESIAN_POINT('Ctrl Pts',(-1.97156914295567,2.85158038765959,8.0241010992273));
#31256=CARTESIAN_POINT('Ctrl Pts',(-3.4658915964548,-0.0786830420698247,
8.18143641489842));
#31257=CARTESIAN_POINT('Ctrl Pts',(-1.84013088404779,-2.93811400679859,
8.33877173056954));
#31258=CARTESIAN_POINT('Ctrl Pts',(1.44216214367922,-3.1525805256303,8.49610704624066));
#31259=CARTESIAN_POINT('Ctrl Pts',(3.42618436209615,-0.529014404638419,
8.6534423619118));
#31260=CARTESIAN_POINT('Ctrl Pts',(2.32586889591107,2.57078382744821,8.81077767758291));
#31261=CARTESIAN_POINT('Ctrl Pts',(-0.868252563983666,3.35629755313536,
8.96811299325404));
#31262=CARTESIAN_POINT('Ctrl Pts',(-3.28075102175166,1.12038736226158,9.12544830892515));
#31263=CARTESIAN_POINT('Ctrl Pts',(-2.73983474254873,-2.12412369627032,
9.28278362459629));
#31264=CARTESIAN_POINT('Ctrl Pts',(0.267550388642249,-3.45644520972622,
9.44011894026741));
#31265=CARTESIAN_POINT('Ctrl Pts',(3.03407913010768,-1.67718692077769,9.59745425593853));
#31266=CARTESIAN_POINT('Ctrl Pts',(3.06925466623264,1.61191643161116,9.75478957160966));
#31267=CARTESIAN_POINT('Ctrl Pts',(0.341406797653059,3.4499337499385,9.91212488728077));
#31268=CARTESIAN_POINT('Ctrl Pts',(-2.69377870488891,2.18223000239878,10.0694602029519));
#31269=CARTESIAN_POINT('Ctrl Pts',(-3.30396687303986,-1.04996552859114,
10.226795518623));
#31270=CARTESIAN_POINT('Ctrl Pts',(-0.939820892206868,-3.33696855340067,
10.3841308342941));
#31271=CARTESIAN_POINT('Ctrl Pts',(2.2703379196763,-2.61992335659027,10.5414661499653));
#31272=CARTESIAN_POINT('Ctrl Pts',(3.43675322554079,0.455595550491001,10.6988014656364));
#31273=CARTESIAN_POINT('Ctrl Pts',(1.50917870869019,3.12106661837885,10.8561367813075));
#31274=CARTESIAN_POINT('Ctrl Pts',(-1.77673321502363,2.97670108175376,11.0134720969786));
#31275=CARTESIAN_POINT('Ctrl Pts',(-3.46368867729937,0.152965991767152,
11.1708074126498));
#31276=CARTESIAN_POINT('Ctrl Pts',(-2.03158068936315,-2.80910804391069,
11.3281427283209));
#31277=CARTESIAN_POINT('Ctrl Pts',(1.22756217529158,-3.24113439556783,11.485478043992));
#31278=CARTESIAN_POINT('Ctrl Pts',(3.38518042007578,-0.757767502188211,
11.6428133596631));
#31279=CARTESIAN_POINT('Ctrl Pts',(2.48830916787281,2.41253151546626,11.8001486753343));
#31280=CARTESIAN_POINT('Ctrl Pts',(0.407565802433691,3.07068338225952,11.9050388857817));
#31281=CARTESIAN_POINT('Ctrl Pts',(-0.545102916878434,2.89105980740811,
11.9574839910054));
#31282=CARTESIAN_POINT('Ctrl Pts',(-2.93989309841074,-0.00232834448912937,
10.1778238829104));
#31283=CARTESIAN_POINT('Ctrl Pts',(-2.94219554736775,-0.304542880453153,
10.1941477614813));
#31284=CARTESIAN_POINT('Ctrl Pts',(-2.89923296915434,-0.606119063222061,
10.2104716400522));
#31285=CARTESIAN_POINT('Ctrl Pts',(-2.80824451487588,-0.892433444227729,
10.226795518623));
#31286=CARTESIAN_POINT('Ctrl Pts',(-2.5159182127622,-1.81229987019432,10.2792406238467));
#31287=CARTESIAN_POINT('Ctrl Pts',(-1.72786955248453,-2.5746342117975,10.3316857290704));
#31288=CARTESIAN_POINT('Ctrl Pts',(-0.798818753698492,-2.83629384979735,
10.3841308342941));
#31289=CARTESIAN_POINT('Ctrl Pts',(0.130232045087536,-3.0979534877972,10.4365759395179));
#31290=CARTESIAN_POINT('Ctrl Pts',(1.20028498238192,-2.85893842219374,10.4890210447416));
#31291=CARTESIAN_POINT('Ctrl Pts',(1.92971400200653,-2.22684440487846,10.5414661499653));
#31292=CARTESIAN_POINT('Ctrl Pts',(2.65914302163113,-1.59475038756318,10.593911255189));
#31293=CARTESIAN_POINT('Ctrl Pts',(3.04794812358597,-0.569577418536059,
10.6463563604127));
#31294=CARTESIAN_POINT('Ctrl Pts',(2.92108825508827,0.387254243958792,10.6988014656364));
#31295=CARTESIAN_POINT('Ctrl Pts',(2.79422838659058,1.34408590645364,10.7512465708601));
#31296=CARTESIAN_POINT('Ctrl Pts',(2.15170354764038,2.23257626241624,10.8036916760838));
#31297=CARTESIAN_POINT('Ctrl Pts',(1.28278914087964,2.6527605176267,10.8561367813075));
#31298=CARTESIAN_POINT('Ctrl Pts',(0.413874734118906,3.07294477283715,10.9085818865312));
#31299=CARTESIAN_POINT('Ctrl Pts',(-0.681429240452357,3.02482292729546,
10.9610269917549));
#31300=CARTESIAN_POINT('Ctrl Pts',(-1.51024047145062,2.53013948952684,11.0134720969786));
#31301=CARTESIAN_POINT('Ctrl Pts',(-1.74480463118476,2.39013776105746,11.0283147313191));
#31302=CARTESIAN_POINT('Ctrl Pts',(-1.95802372783935,2.21436813426865,11.0431573656595));
#31303=CARTESIAN_POINT('Ctrl Pts',(-2.14415473270596,2.01243073062332,11.058));
#31304=CARTESIAN_POINT('Ctrl Pts',(-1.37989654081095,-1.933266887693,1.56125112837913E-17));
#31305=CARTESIAN_POINT('Ctrl Pts',(-1.44414345926609,-1.89839188587405,
5.80920822621902E-18));
#31306=CARTESIAN_POINT('Ctrl Pts',(-1.5065284577229,-1.86047032724736,-1.41833741640826E-16));
#31307=CARTESIAN_POINT('Ctrl Pts',(-1.56680444439783,-1.81955553349441,
-1.49186218934005E-16));
#31308=CARTESIAN_POINT('Ctrl Pts',(-1.63448180748404,-1.77361675247786,
-1.62745475426733E-16));
#31309=CARTESIAN_POINT('Ctrl Pts',(-1.69950176926845,-1.72390575990714,
4.47554715783556E-16));
#31310=CARTESIAN_POINT('Ctrl Pts',(-1.76178079551988,-1.6707784873017,5.27355936696949E-16));
#31311=CARTESIAN_POINT('Ctrl Pts',(-1.80277525259689,-1.63580806744237,
5.79884178102324E-16));
#31312=CARTESIAN_POINT('Ctrl Pts',(-1.84258178887229,-1.59935636303953,
9.13682232518509E-17));
#31313=CARTESIAN_POINT('Ctrl Pts',(-1.88117141744704,-1.56151405921777,
1.59594559789866E-16));
#31314=CARTESIAN_POINT('Ctrl Pts',(-1.89157558896771,-1.55131137434519,
1.77989100856589E-16));
#31315=CARTESIAN_POINT('Ctrl Pts',(-1.90188938652621,-1.54100934347453,
3.40635361961997E-16));
#31316=CARTESIAN_POINT('Ctrl Pts',(-1.91210630257196,-1.53061605927472,
3.05311331771918E-16));
#31317=CARTESIAN_POINT('Ctrl Pts',(-1.9724409846318,-1.46923985779222,9.67098202152561E-17));
#31318=CARTESIAN_POINT('Ctrl Pts',(-2.02946085491381,-1.40462521591101,
1.4935214824922E-16));
#31319=CARTESIAN_POINT('Ctrl Pts',(-2.08307562783518,-1.33717477526203,
1.38777878078145E-16));
#31320=CARTESIAN_POINT('Ctrl Pts',(-2.12998855414138,-1.27815563969417,
1.29525391678454E-16));
#31321=CARTESIAN_POINT('Ctrl Pts',(-2.17429437900105,-1.21696417926775,
2.01441503266146E-16));
#31322=CARTESIAN_POINT('Ctrl Pts',(-2.21591583956505,-1.15384057343859,
1.52655665885959E-16));
#31323=CARTESIAN_POINT('Ctrl Pts',(-2.23664963326987,-1.12239545345888,
1.28352927004359E-16));
#31324=CARTESIAN_POINT('Ctrl Pts',(-2.25671701785544,-1.09047047206691,
-2.37280165770185E-16));
#31325=CARTESIAN_POINT('Ctrl Pts',(-2.2761066605572,-1.05809323638609,-2.63677968348475E-16));
#31326=CARTESIAN_POINT('Ctrl Pts',(-2.28578146762193,-1.0419380388242,-2.76849621421526E-16));
#31327=CARTESIAN_POINT('Ctrl Pts',(-2.29528887628369,-1.02566760843717,
-1.10809144900277E-17));
#31328=CARTESIAN_POINT('Ctrl Pts',(-2.30461525834334,-1.0093071858719,0.));
#31329=CARTESIAN_POINT('Ctrl Pts',(-2.34846766322256,-0.932380906234359,
5.21021705459412E-17));
#31330=CARTESIAN_POINT('Ctrl Pts',(-2.38837887518559,-0.853373340579809,
-1.59588577561705E-17));
#31331=CARTESIAN_POINT('Ctrl Pts',(-2.42425706703596,-0.772682188207588,
-2.77555756156289E-17));
#31332=CARTESIAN_POINT('Ctrl Pts',(-2.46075963346513,-0.690586798283878,
-3.97575872863117E-17));
#31333=CARTESIAN_POINT('Ctrl Pts',(-2.49308822244858,-0.606748001409621,
2.24945356107799E-18));
#31334=CARTESIAN_POINT('Ctrl Pts',(-2.52111243497218,-0.521542915861604,
-2.77555756156289E-17));
#31335=CARTESIAN_POINT('Ctrl Pts',(-2.54406484395513,-0.4517581906252,-5.23303143573299E-17));
#31336=CARTESIAN_POINT('Ctrl Pts',(-2.56412941494483,-0.381055975787894,
-5.2234519399031E-17));
#31337=CARTESIAN_POINT('Ctrl Pts',(-2.58121358727312,-0.309628512371508,
-5.55111512312578E-17));
#31338=CARTESIAN_POINT('Ctrl Pts',(-2.59402671651933,-0.256057914809218,
-5.79686251054279E-17));
#31339=CARTESIAN_POINT('Ctrl Pts',(-2.6051630020304,-0.202079063721199,
-1.68485553630616E-16));
#31340=CARTESIAN_POINT('Ctrl Pts',(-2.61457527537642,-0.147769877191515,
-1.94289029309402E-16));
#31341=CARTESIAN_POINT('Ctrl Pts',(-2.617136534184,-0.132991313371873,-2.01310646395843E-16));
#31342=CARTESIAN_POINT('Ctrl Pts',(-2.6195700893165,-0.118188277474481,
-3.31395093795537E-16));
#31343=CARTESIAN_POINT('Ctrl Pts',(-2.6218748923051,-0.103362317982878,
-3.33066907387547E-16));
#31344=CARTESIAN_POINT('Ctrl Pts',(-2.62397146608191,-0.089875821288789,
-3.34587679685255E-16));
#31345=CARTESIAN_POINT('Ctrl Pts',(-2.62596008221826,-0.076379405564125,
-2.78772373994456E-16));
#31346=CARTESIAN_POINT('Ctrl Pts',(-2.62784009463941,-0.0628763941457686,
-2.77555756156289E-16));
#31347=CARTESIAN_POINT('Ctrl Pts',(-2.64060982150785,0.0288409614284714,
-2.69292046128659E-16));
#31348=CARTESIAN_POINT('Ctrl Pts',(-2.64837710873961,0.12089024959815,-1.76997536955934E-16));
#31349=CARTESIAN_POINT('Ctrl Pts',(-2.65101366112809,0.212875307143708,
-1.38777878078145E-16));
#31350=CARTESIAN_POINT('Ctrl Pts',(-2.65226659852151,0.256588270610049,
-1.20615204739669E-16));
#31351=CARTESIAN_POINT('Ctrl Pts',(-2.65236023741492,0.300287183221066,
-4.34987190636111E-16));
#31352=CARTESIAN_POINT('Ctrl Pts',(-2.6512772014093,0.343931535522003,-4.16333634234434E-16));
#31353=CARTESIAN_POINT('Ctrl Pts',(-2.64907421925761,0.432707650667494,
-4.32903459206313E-16));
#31354=CARTESIAN_POINT('Ctrl Pts',(-2.64200629387468,0.521257644934972,
-8.62622134822235E-17));
#31355=CARTESIAN_POINT('Ctrl Pts',(-2.63031624428264,0.609320814221094,
-8.32667268468867E-17));
#31356=CARTESIAN_POINT('Ctrl Pts',(-2.61839797794639,0.699103179787949,
-8.02127613999854E-17));
#31357=CARTESIAN_POINT('Ctrl Pts',(-2.60167524897612,0.788380265268053,
1.49019320792917E-16));
#31358=CARTESIAN_POINT('Ctrl Pts',(-2.58035146554209,0.876878238745711,
2.4980018054066E-16));
#31359=CARTESIAN_POINT('Ctrl Pts',(-2.57698234718955,0.890860754912604,
2.65723370025807E-16));
#31360=CARTESIAN_POINT('Ctrl Pts',(-2.57349826551832,0.904823813068977,
1.71128026421916E-16));
#31361=CARTESIAN_POINT('Ctrl Pts',(-2.56989990586492,0.918766319054272,
1.94289029309402E-16));
#31362=CARTESIAN_POINT('Ctrl Pts',(-2.56629916621592,0.932718046770052,
2.17465351145046E-16));
#31363=CARTESIAN_POINT('Ctrl Pts',(-2.56258611805641,0.946640891227604,
-7.03868084514403E-16));
#31364=CARTESIAN_POINT('Ctrl Pts',(-2.55876298044222,0.960529869852388,
-6.93889390390723E-16));
#31365=CARTESIAN_POINT('Ctrl Pts',(-2.53419843880054,1.04976976342104,-6.29773977327716E-16));
#31366=CARTESIAN_POINT('Ctrl Pts',(-2.50508011125346,1.13766264916498,6.87890529294335E-17));
#31367=CARTESIAN_POINT('Ctrl Pts',(-2.47169823504828,1.22392740477737,8.32667268468867E-17));
#31368=CARTESIAN_POINT('Ctrl Pts',(-2.43767482619284,1.31184999582573,9.80226325947151E-17));
#31369=CARTESIAN_POINT('Ctrl Pts',(-2.39922225163329,1.39808205966622,-2.50151931196036E-16));
#31370=CARTESIAN_POINT('Ctrl Pts',(-2.35659236008881,1.48232869936419,-2.77555756156289E-16));
#31371=CARTESIAN_POINT('Ctrl Pts',(-2.31360056696885,1.56729054124849,-3.05192222745878E-16));
#31372=CARTESIAN_POINT('Ctrl Pts',(-2.26635993703635,1.65023397727082,5.65740922539343E-17));
#31373=CARTESIAN_POINT('Ctrl Pts',(-2.21507658716517,1.73084671943837,5.55111512312578E-17));
#31374=CARTESIAN_POINT('Ctrl Pts',(-2.18435464293681,1.77913880985734,5.48743828668913E-17));
#31375=CARTESIAN_POINT('Ctrl Pts',(-2.15218088295609,1.82659422289983,-3.64380860772878E-16));
#31376=CARTESIAN_POINT('Ctrl Pts',(-2.11859145320912,1.87314213253736,-3.88578058618805E-16));
#31377=CARTESIAN_POINT('Ctrl Pts',(-2.10923966749503,1.88610174750099,-3.95314910385597E-16));
#31378=CARTESIAN_POINT('Ctrl Pts',(-2.09977706809611,1.89899226435558,-9.16981750261902E-17));
#31379=CARTESIAN_POINT('Ctrl Pts',(-2.0902160744712,1.91179680016256,-1.11022302462516E-16));
#31380=CARTESIAN_POINT('Ctrl Pts',(-2.03140899114824,1.99055403331781,-2.29879778669894E-16));
#31381=CARTESIAN_POINT('Ctrl Pts',(-1.96879105165951,2.06618994280669,4.68887291460301E-17));
#31382=CARTESIAN_POINT('Ctrl Pts',(-1.90263522085423,2.13839704217079,0.));
#31383=CARTESIAN_POINT('Ctrl Pts',(-1.83630675569242,2.21079256674222,-4.70110857922477E-17));
#31384=CARTESIAN_POINT('Ctrl Pts',(-1.76642150904269,2.27974226115238,-1.93865480317173E-16));
#31385=CARTESIAN_POINT('Ctrl Pts',(-1.6932045763485,2.34492041918897,-1.66533453693773E-16));
#31386=CARTESIAN_POINT('Ctrl Pts',(-1.62138195170811,2.40885735573024,-1.39721925040515E-16));
#31387=CARTESIAN_POINT('Ctrl Pts',(-1.54635279514513,2.46916580377976,-2.38947154895597E-16));
#31388=CARTESIAN_POINT('Ctrl Pts',(-1.46828869930752,2.52551090354043,-2.77555756156289E-16));
#31389=CARTESIAN_POINT('Ctrl Pts',(-1.41016377964657,2.56746430557163,-3.06302926317174E-16));
#31390=CARTESIAN_POINT('Ctrl Pts',(-1.35035542782446,2.60721994910279,8.78385754915914E-18));
#31391=CARTESIAN_POINT('Ctrl Pts',(-1.28892185405322,2.64462557919718,0.));
#31392=CARTESIAN_POINT('Origin',(0.,0.,0.));
#31393=CARTESIAN_POINT('Origin',(-1.44337567297407,-2.5,-6.));
#31394=CARTESIAN_POINT('',(-1.44337567297407,-2.5,-6.));
#31395=CARTESIAN_POINT('',(1.44337567297406,-2.5,-6.));
#31396=CARTESIAN_POINT('',(-0.721687836487033,-2.5,-6.));
#31397=CARTESIAN_POINT('',(-1.44337567297407,-2.5,-3.));
#31398=CARTESIAN_POINT('',(-1.44337567297407,-2.5,-6.));
#31399=CARTESIAN_POINT('',(1.44337567297406,-2.5,-3.));
#31400=CARTESIAN_POINT('',(-1.44337567297407,-2.5,-3.));
#31401=CARTESIAN_POINT('',(1.44337567297406,-2.5,-6.));
#31402=CARTESIAN_POINT('Origin',(-2.88675134594813,3.53525079574969E-16,
-6.));
#31403=CARTESIAN_POINT('',(-2.88675134594813,3.53525079574969E-16,-6.));
#31404=CARTESIAN_POINT('',(-2.52590742770461,-0.625,-6.));
#31405=CARTESIAN_POINT('',(-2.88675134594813,5.55111512312578E-16,-3.));
#31406=CARTESIAN_POINT('',(-2.88675134594813,3.53525079574969E-16,-6.));
#31407=CARTESIAN_POINT('',(-2.88675134594813,3.53525079574969E-16,-3.));
#31408=CARTESIAN_POINT('Origin',(-1.44337567297406,2.5,-6.));
#31409=CARTESIAN_POINT('',(-1.44337567297406,2.5,-6.));
#31410=CARTESIAN_POINT('',(-1.80421959121758,1.875,-6.));
#31411=CARTESIAN_POINT('',(-1.44337567297406,2.5,-3.));
#31412=CARTESIAN_POINT('',(-1.44337567297406,2.5,-6.));
#31413=CARTESIAN_POINT('',(-1.44337567297406,2.5,-3.));
#31414=CARTESIAN_POINT('Origin',(1.44337567297406,2.5,-6.));
#31415=CARTESIAN_POINT('',(1.44337567297406,2.5,-6.));
#31416=CARTESIAN_POINT('',(0.721687836487033,2.5,-6.));
#31417=CARTESIAN_POINT('',(1.44337567297406,2.5,-3.));
#31418=CARTESIAN_POINT('',(1.44337567297406,2.5,-6.));
#31419=CARTESIAN_POINT('',(1.44337567297406,2.5,-3.));
#31420=CARTESIAN_POINT('Origin',(2.88675134594813,0.,-6.));
#31421=CARTESIAN_POINT('',(2.88675134594813,0.,-6.));
#31422=CARTESIAN_POINT('',(2.52590742770461,0.625,-6.));
#31423=CARTESIAN_POINT('',(2.88675134594813,0.,-3.));
#31424=CARTESIAN_POINT('',(2.88675134594813,0.,-6.));
#31425=CARTESIAN_POINT('',(2.88675134594813,0.,-3.));
#31426=CARTESIAN_POINT('Origin',(1.44337567297406,-2.5,-6.));
#31427=CARTESIAN_POINT('',(1.80421959121758,-1.875,-6.));
#31428=CARTESIAN_POINT('',(1.44337567297406,-2.5,-3.));
#31429=CARTESIAN_POINT('Origin',(0.,0.,-3.));
#31430=CARTESIAN_POINT('Origin',(0.,0.,0.));
#31431=CARTESIAN_POINT('',(-5.,-6.12323399573677E-16,0.));
#31432=CARTESIAN_POINT('Origin',(0.,0.,0.));
#31433=CARTESIAN_POINT('Origin',(0.,0.,-6.));
#31434=CARTESIAN_POINT('',(-5.,-6.12323399573677E-16,-6.));
#31435=CARTESIAN_POINT('',(-5.,-6.12323399573677E-16,-6.));
#31436=CARTESIAN_POINT('Origin',(0.,0.,-6.));
#31437=CARTESIAN_POINT('Origin',(0.,0.,-6.));
#31438=CARTESIAN_POINT('Origin',(0.,0.,12.));
#32604=UNCERTAINTY_MEASURE_WITH_UNIT(LENGTH_MEASURE(0.01),#32628,
'DISTANCE_ACCURACY_VALUE',
'Maximum model space distance between geometric entities at asserted c
onnectivities');
#32607=UNCERTAINTY_MEASURE_WITH_UNIT(LENGTH_MEASURE(0.01),#32628,
'DISTANCE_ACCURACY_VALUE',
'Maximum model space distance between geometric entities at asserted c
onnectivities');
#32624=(
GEOMETRIC_REPRESENTATION_CONTEXT(3)
GLOBAL_UNCERTAINTY_ASSIGNED_CONTEXT((#32604))
GLOBAL_UNIT_ASSIGNED_CONTEXT((#32628,#32630,#32631))
REPRESENTATION_CONTEXT('','3D')
);
#32627=(
GEOMETRIC_REPRESENTATION_CONTEXT(3)
GLOBAL_UNCERTAINTY_ASSIGNED_CONTEXT((#32607))
GLOBAL_UNIT_ASSIGNED_CONTEXT((#32628,#32630,#32631))
REPRESENTATION_CONTEXT('','3D')
);
#32628=(
LENGTH_UNIT()
NAMED_UNIT(*)
SI_UNIT(.MILLI.,.METRE.)
);
#32630=(
NAMED_UNIT(*)
PLANE_ANGLE_UNIT()
SI_UNIT($,.RADIAN.)
);
#32631=(
NAMED_UNIT(*)
SI_UNIT($,.STERADIAN.)
SOLID_ANGLE_UNIT()
);
#32648=SHAPE_DEFINITION_REPRESENTATION(#32667,#32723);
#32667=PRODUCT_DEFINITION_SHAPE('',$,#32743);
#32723=SHAPE_REPRESENTATION('',(#9414),#32624);
#32726=PRODUCT_DEFINITION_CONTEXT('part definition',#32785,'design');
#32743=PRODUCT_DEFINITION('Socket head cap screw M6x12',
'Socket head cap screw M6x12',#32762,#32726);
#32762=PRODUCT_DEFINITION_FORMATION('',$,#32803);
#32785=APPLICATION_CONTEXT(
'Core Data for Automotive Mechanical Design Process');
#32786=PRODUCT_CONTEXT('part definition',#32785,'mechanical');
#32803=PRODUCT('Socket head cap screw M6x12',
'Socket head cap screw M6x12',$,(#32786));
#32809=PRESENTATION_STYLE_ASSIGNMENT((#32816));
#32816=SURFACE_STYLE_USAGE(.BOTH.,#32823);
#32823=SURFACE_SIDE_STYLE('',(#32830));
#32830=SURFACE_STYLE_FILL_AREA(#32837);
#32837=FILL_AREA_STYLE('Dark gray',(#32844));
#32844=FILL_AREA_STYLE_COLOUR('Dark gray',#32851);
#32851=COLOUR_RGB('Dark gray',0.250980392156863,0.282352941176471,0.32156862745098);
ENDSEC;
END-ISO-10303-21;
